ISO-10303-21;
HEADER;
/* Generated by software containing ST-Developer
 * from STEP Tools, Inc. (www.steptools.com) 
 */

FILE_DESCRIPTION(
/* description */ (''),
/* implementation_level */ '2;1');

FILE_NAME(
/* name */ 'Bottom_Plate.step',
/* time_stamp */ '2026-10-22T13:39:42+06:00',
/* author */ (''),
/* organization */ (''),
/* preprocessor_version */ 'ST-DEVELOPER v20.2',
/* originating_system */ 'Autodesk Translation Framework v15.15.0.0',
/* authorisation */ '');

FILE_SCHEMA (('AUTOMOTIVE_DESIGN { 1 0 10303 214 3 1 1 }'));
ENDSEC;

DATA;
#10=MECHANICAL_DESIGN_GEOMETRIC_PRESENTATION_REPRESENTATION('',(#308),#17836);
#119=SPHERICAL_SURFACE('',#9812,0.499999999999998);
#120=SPHERICAL_SURFACE('',#9816,0.499999999999998);
#121=SPHERICAL_SURFACE('',#9821,0.5);
#122=SPHERICAL_SURFACE('',#9827,0.499999999999998);
#123=SPHERICAL_SURFACE('',#9837,0.500000000000007);
#124=SPHERICAL_SURFACE('',#9846,0.500000000000007);
#125=SPHERICAL_SURFACE('',#9859,0.5);
#126=SPHERICAL_SURFACE('',#9863,0.5);
#127=SPHERICAL_SURFACE('',#9868,0.5);
#128=SPHERICAL_SURFACE('',#9874,0.5);
#129=SPHERICAL_SURFACE('',#9883,0.500000000000007);
#130=SPHERICAL_SURFACE('',#9891,0.500000000000007);
#131=SPHERICAL_SURFACE('',#9896,0.500000000000007);
#132=SPHERICAL_SURFACE('',#9902,0.499999999999998);
#211=TOROIDAL_SURFACE('',#9804,0.999999999999996,0.500000000000007);
#212=TOROIDAL_SURFACE('',#9808,1.,0.500000000000007);
#213=TOROIDAL_SURFACE('',#9833,0.999999999999996,0.500000000000007);
#214=TOROIDAL_SURFACE('',#9840,1.,0.500000000000007);
#215=TOROIDAL_SURFACE('',#9849,1.,0.500000000000007);
#216=TOROIDAL_SURFACE('',#9853,1.,0.500000000000007);
#217=TOROIDAL_SURFACE('',#9879,0.99999999999999,0.500000000000007);
#218=TOROIDAL_SURFACE('',#9887,0.999999999999994,0.5);
#267=ELLIPSE('',#9773,0.707106781186543,0.5);
#268=ELLIPSE('',#9779,0.707106781186553,0.5);
#288=SHAPE_REPRESENTATION_RELATIONSHIP('SRR','None',#17875,#298);
#298=ADVANCED_BREP_SHAPE_REPRESENTATION('',(#318),#17827);
#308=STYLED_ITEM('',(#17959),#318);
#318=MANIFOLD_SOLID_BREP('Bottom_Plate',#9629);
#329=CYLINDRICAL_SURFACE('',#9772,0.5);
#330=CYLINDRICAL_SURFACE('',#9774,0.5);
#331=CYLINDRICAL_SURFACE('',#9778,0.5);
#332=CYLINDRICAL_SURFACE('',#9780,0.5);
#333=CYLINDRICAL_SURFACE('',#9794,0.5);
#334=CYLINDRICAL_SURFACE('',#9802,0.5);
#335=CYLINDRICAL_SURFACE('',#9820,0.5);
#336=CYLINDRICAL_SURFACE('',#9825,0.5);
#337=CYLINDRICAL_SURFACE('',#9826,0.5);
#338=CYLINDRICAL_SURFACE('',#9831,0.5);
#339=CYLINDRICAL_SURFACE('',#9832,0.5);
#340=CYLINDRICAL_SURFACE('',#9844,0.5);
#341=CYLINDRICAL_SURFACE('',#9845,0.5);
#342=CYLINDRICAL_SURFACE('',#9857,0.5);
#343=CYLINDRICAL_SURFACE('',#9858,0.5);
#344=CYLINDRICAL_SURFACE('',#9867,0.5);
#345=CYLINDRICAL_SURFACE('',#9872,0.5);
#346=CYLINDRICAL_SURFACE('',#9873,0.5);
#347=CYLINDRICAL_SURFACE('',#9877,0.5);
#348=CYLINDRICAL_SURFACE('',#9878,0.5);
#349=CYLINDRICAL_SURFACE('',#9886,0.5);
#350=CYLINDRICAL_SURFACE('',#9895,0.5);
#351=CYLINDRICAL_SURFACE('',#9900,0.5);
#352=CYLINDRICAL_SURFACE('',#9901,0.5);
#353=CYLINDRICAL_SURFACE('',#9906,0.5);
#354=CYLINDRICAL_SURFACE('',#9907,0.5);
#355=CYLINDRICAL_SURFACE('',#9908,0.5);
#356=CYLINDRICAL_SURFACE('',#9909,0.5);
#357=CYLINDRICAL_SURFACE('',#9910,0.5);
#358=CYLINDRICAL_SURFACE('',#9911,0.5);
#359=CYLINDRICAL_SURFACE('',#9912,0.5);
#360=CYLINDRICAL_SURFACE('',#9913,0.5);
#361=CYLINDRICAL_SURFACE('',#9914,0.5);
#362=CYLINDRICAL_SURFACE('',#9915,0.5);
#363=CYLINDRICAL_SURFACE('',#9916,0.5);
#364=CYLINDRICAL_SURFACE('',#9917,0.5);
#365=CYLINDRICAL_SURFACE('',#9918,0.5);
#366=CYLINDRICAL_SURFACE('',#9919,0.5);
#367=CYLINDRICAL_SURFACE('',#9920,0.5);
#644=LINE('',#14294,#1309);
#645=LINE('',#14296,#1310);
#646=LINE('',#14298,#1311);
#647=LINE('',#14301,#1312);
#648=LINE('',#14307,#1313);
#649=LINE('',#14311,#1314);
#650=LINE('',#14313,#1315);
#651=LINE('',#14314,#1316);
#652=LINE('',#14316,#1317);
#653=LINE('',#14317,#1318);
#654=LINE('',#14320,#1319);
#655=LINE('',#14323,#1320);
#656=LINE('',#14326,#1321);
#657=LINE('',#14329,#1322);
#658=LINE('',#14332,#1323);
#659=LINE('',#14333,#1324);
#660=LINE('',#14336,#1325);
#661=LINE('',#14337,#1326);
#662=LINE('',#14341,#1327);
#663=LINE('',#14344,#1328);
#664=LINE('',#14348,#1329);
#665=LINE('',#14350,#1330);
#666=LINE('',#14352,#1331);
#667=LINE('',#14354,#1332);
#668=LINE('',#14356,#1333);
#669=LINE('',#14358,#1334);
#670=LINE('',#14360,#1335);
#671=LINE('',#14362,#1336);
#672=LINE('',#14366,#1337);
#673=LINE('',#14368,#1338);
#674=LINE('',#14372,#1339);
#675=LINE('',#14376,#1340);
#676=LINE('',#14378,#1341);
#677=LINE('',#14382,#1342);
#678=LINE('',#14383,#1343);
#679=LINE('',#14388,#1344);
#680=LINE('',#14390,#1345);
#681=LINE('',#14393,#1346);
#682=LINE('',#14398,#1347);
#683=LINE('',#14402,#1348);
#684=LINE('',#14403,#1349);
#685=LINE('',#14405,#1350);
#686=LINE('',#14408,#1351);
#687=LINE('',#14412,#1352);
#688=LINE('',#14414,#1353);
#689=LINE('',#14418,#1354);
#690=LINE('',#14420,#1355);
#691=LINE('',#14424,#1356);
#692=LINE('',#14428,#1357);
#693=LINE('',#14430,#1358);
#694=LINE('',#14434,#1359);
#695=LINE('',#14436,#1360);
#696=LINE('',#14437,#1361);
#697=LINE('',#14439,#1362);
#698=LINE('',#14440,#1363);
#699=LINE('',#14443,#1364);
#700=LINE('',#14444,#1365);
#701=LINE('',#14447,#1366);
#702=LINE('',#14474,#1367);
#703=LINE('',#14482,#1368);
#704=LINE('',#14484,#1369);
#705=LINE('',#14485,#1370);
#706=LINE('',#14493,#1371);
#707=LINE('',#14494,#1372);
#708=LINE('',#14496,#1373);
#709=LINE('',#14514,#1374);
#710=LINE('',#14516,#1375);
#711=LINE('',#14517,#1376);
#712=LINE('',#14535,#1377);
#713=LINE('',#14537,#1378);
#714=LINE('',#14538,#1379);
#715=LINE('',#14552,#1380);
#716=LINE('',#14560,#1381);
#717=LINE('',#14562,#1382);
#718=LINE('',#14563,#1383);
#719=LINE('',#14569,#1384);
#720=LINE('',#14570,#1385);
#721=LINE('',#14572,#1386);
#722=LINE('',#14584,#1387);
#723=LINE('',#14604,#1388);
#724=LINE('',#14606,#1389);
#725=LINE('',#14614,#1390);
#726=LINE('',#14615,#1391);
#727=LINE('',#14617,#1392);
#728=LINE('',#14619,#1393);
#729=LINE('',#14621,#1394);
#730=LINE('',#14623,#1395);
#731=LINE('',#14625,#1396);
#732=LINE('',#14626,#1397);
#733=LINE('',#14628,#1398);
#734=LINE('',#14630,#1399);
#735=LINE('',#14632,#1400);
#736=LINE('',#14634,#1401);
#737=LINE('',#14636,#1402);
#738=LINE('',#14638,#1403);
#739=LINE('',#14640,#1404);
#740=LINE('',#14642,#1405);
#741=LINE('',#14644,#1406);
#742=LINE('',#14645,#1407);
#1309=VECTOR('',#11072,10.);
#1310=VECTOR('',#11073,10.);
#1311=VECTOR('',#11074,10.);
#1312=VECTOR('',#11077,10.);
#1313=VECTOR('',#11082,10.);
#1314=VECTOR('',#11085,10.);
#1315=VECTOR('',#11086,10.);
#1316=VECTOR('',#11087,10.);
#1317=VECTOR('',#11090,10.);
#1318=VECTOR('',#11091,10.);
#1319=VECTOR('',#11094,10.);
#1320=VECTOR('',#11097,10.);
#1321=VECTOR('',#11100,10.);
#1322=VECTOR('',#11103,10.);
#1323=VECTOR('',#11106,10.);
#1324=VECTOR('',#11107,10.);
#1325=VECTOR('',#11110,10.);
#1326=VECTOR('',#11111,10.);
#1327=VECTOR('',#11116,10.);
#1328=VECTOR('',#11119,10.);
#1329=VECTOR('',#11124,10.);
#1330=VECTOR('',#11125,10.);
#1331=VECTOR('',#11126,10.);
#1332=VECTOR('',#11127,10.);
#1333=VECTOR('',#11128,10.);
#1334=VECTOR('',#11129,10.);
#1335=VECTOR('',#11130,10.);
#1336=VECTOR('',#11131,10.);
#1337=VECTOR('',#11134,10.);
#1338=VECTOR('',#11135,10.);
#1339=VECTOR('',#11138,10.);
#1340=VECTOR('',#11141,10.);
#1341=VECTOR('',#11142,10.);
#1342=VECTOR('',#11145,10.);
#1343=VECTOR('',#11146,10.);
#1344=VECTOR('',#11151,10.);
#1345=VECTOR('',#11152,10.);
#1346=VECTOR('',#11155,10.);
#1347=VECTOR('',#11160,10.);
#1348=VECTOR('',#11163,10.);
#1349=VECTOR('',#11164,10.);
#1350=VECTOR('',#11167,10.);
#1351=VECTOR('',#11170,10.);
#1352=VECTOR('',#11175,10.);
#1353=VECTOR('',#11176,10.);
#1354=VECTOR('',#11179,10.);
#1355=VECTOR('',#11180,10.);
#1356=VECTOR('',#11183,10.);
#1357=VECTOR('',#11186,10.);
#1358=VECTOR('',#11187,10.);
#1359=VECTOR('',#11190,10.);
#1360=VECTOR('',#11191,10.);
#1361=VECTOR('',#11192,10.);
#1362=VECTOR('',#11193,10.);
#1363=VECTOR('',#11194,10.);
#1364=VECTOR('',#11197,10.);
#1365=VECTOR('',#11198,10.);
#1366=VECTOR('',#11201,10.);
#1367=VECTOR('',#11238,10.);
#1368=VECTOR('',#11249,10.);
#1369=VECTOR('',#11252,10.);
#1370=VECTOR('',#11253,10.);
#1371=VECTOR('',#11264,10.);
#1372=VECTOR('',#11265,10.);
#1373=VECTOR('',#11268,10.);
#1374=VECTOR('',#11293,10.);
#1375=VECTOR('',#11296,10.);
#1376=VECTOR('',#11297,10.);
#1377=VECTOR('',#11322,10.);
#1378=VECTOR('',#11325,10.);
#1379=VECTOR('',#11326,10.);
#1380=VECTOR('',#11345,10.);
#1381=VECTOR('',#11356,10.);
#1382=VECTOR('',#11359,10.);
#1383=VECTOR('',#11360,10.);
#1384=VECTOR('',#11369,10.);
#1385=VECTOR('',#11370,10.);
#1386=VECTOR('',#11373,10.);
#1387=VECTOR('',#11390,10.);
#1388=VECTOR('',#11419,10.);
#1389=VECTOR('',#11422,10.);
#1390=VECTOR('',#11433,10.);
#1391=VECTOR('',#11434,10.);
#1392=VECTOR('',#11437,10.);
#1393=VECTOR('',#11440,10.);
#1394=VECTOR('',#11443,10.);
#1395=VECTOR('',#11446,10.);
#1396=VECTOR('',#11449,10.);
#1397=VECTOR('',#11450,10.);
#1398=VECTOR('',#11453,10.);
#1399=VECTOR('',#11456,10.);
#1400=VECTOR('',#11459,10.);
#1401=VECTOR('',#11462,10.);
#1402=VECTOR('',#11465,10.);
#1403=VECTOR('',#11468,10.);
#1404=VECTOR('',#11471,10.);
#1405=VECTOR('',#11474,10.);
#1406=VECTOR('',#11477,10.);
#1407=VECTOR('',#11478,10.);
#2034=FACE_OUTER_BOUND('',#2649,.T.);
#2035=FACE_OUTER_BOUND('',#2650,.T.);
#2036=FACE_OUTER_BOUND('',#2651,.T.);
#2037=FACE_OUTER_BOUND('',#2652,.T.);
#2038=FACE_OUTER_BOUND('',#2653,.T.);
#2039=FACE_OUTER_BOUND('',#2654,.T.);
#2040=FACE_OUTER_BOUND('',#2655,.T.);
#2041=FACE_OUTER_BOUND('',#2656,.T.);
#2042=FACE_OUTER_BOUND('',#2657,.T.);
#2043=FACE_OUTER_BOUND('',#2658,.T.);
#2044=FACE_OUTER_BOUND('',#2659,.T.);
#2045=FACE_OUTER_BOUND('',#2660,.T.);
#2046=FACE_OUTER_BOUND('',#2661,.T.);
#2047=FACE_OUTER_BOUND('',#2662,.T.);
#2048=FACE_OUTER_BOUND('',#2663,.T.);
#2049=FACE_OUTER_BOUND('',#2664,.T.);
#2050=FACE_OUTER_BOUND('',#2665,.T.);
#2051=FACE_OUTER_BOUND('',#2666,.T.);
#2052=FACE_OUTER_BOUND('',#2667,.T.);
#2053=FACE_OUTER_BOUND('',#2668,.T.);
#2054=FACE_OUTER_BOUND('',#2669,.T.);
#2055=FACE_OUTER_BOUND('',#2670,.T.);
#2056=FACE_OUTER_BOUND('',#2671,.T.);
#2057=FACE_OUTER_BOUND('',#2672,.T.);
#2058=FACE_OUTER_BOUND('',#2673,.T.);
#2059=FACE_OUTER_BOUND('',#2674,.T.);
#2060=FACE_OUTER_BOUND('',#2675,.T.);
#2061=FACE_OUTER_BOUND('',#2676,.T.);
#2062=FACE_OUTER_BOUND('',#2677,.T.);
#2063=FACE_OUTER_BOUND('',#2678,.T.);
#2064=FACE_OUTER_BOUND('',#2679,.T.);
#2065=FACE_OUTER_BOUND('',#2680,.T.);
#2066=FACE_OUTER_BOUND('',#2681,.T.);
#2067=FACE_OUTER_BOUND('',#2682,.T.);
#2068=FACE_OUTER_BOUND('',#2683,.T.);
#2069=FACE_OUTER_BOUND('',#2684,.T.);
#2070=FACE_OUTER_BOUND('',#2685,.T.);
#2071=FACE_OUTER_BOUND('',#2686,.T.);
#2072=FACE_OUTER_BOUND('',#2687,.T.);
#2073=FACE_OUTER_BOUND('',#2688,.T.);
#2074=FACE_OUTER_BOUND('',#2689,.T.);
#2075=FACE_OUTER_BOUND('',#2690,.T.);
#2076=FACE_OUTER_BOUND('',#2691,.T.);
#2077=FACE_OUTER_BOUND('',#2692,.T.);
#2078=FACE_OUTER_BOUND('',#2693,.T.);
#2079=FACE_OUTER_BOUND('',#2694,.T.);
#2080=FACE_OUTER_BOUND('',#2695,.T.);
#2081=FACE_OUTER_BOUND('',#2696,.T.);
#2082=FACE_OUTER_BOUND('',#2697,.T.);
#2083=FACE_OUTER_BOUND('',#2698,.T.);
#2084=FACE_OUTER_BOUND('',#2699,.T.);
#2085=FACE_OUTER_BOUND('',#2700,.T.);
#2086=FACE_OUTER_BOUND('',#2701,.T.);
#2087=FACE_OUTER_BOUND('',#2702,.T.);
#2088=FACE_OUTER_BOUND('',#2703,.T.);
#2089=FACE_OUTER_BOUND('',#2704,.T.);
#2090=FACE_OUTER_BOUND('',#2705,.T.);
#2091=FACE_OUTER_BOUND('',#2706,.T.);
#2092=FACE_OUTER_BOUND('',#2707,.T.);
#2093=FACE_OUTER_BOUND('',#2708,.T.);
#2094=FACE_OUTER_BOUND('',#2709,.T.);
#2095=FACE_OUTER_BOUND('',#2710,.T.);
#2096=FACE_OUTER_BOUND('',#2711,.T.);
#2097=FACE_OUTER_BOUND('',#2712,.T.);
#2098=FACE_OUTER_BOUND('',#2713,.T.);
#2099=FACE_OUTER_BOUND('',#2714,.T.);
#2100=FACE_OUTER_BOUND('',#2715,.T.);
#2101=FACE_OUTER_BOUND('',#2716,.T.);
#2102=FACE_OUTER_BOUND('',#2717,.T.);
#2103=FACE_OUTER_BOUND('',#2718,.T.);
#2104=FACE_OUTER_BOUND('',#2719,.T.);
#2105=FACE_OUTER_BOUND('',#2720,.T.);
#2106=FACE_OUTER_BOUND('',#2721,.T.);
#2107=FACE_OUTER_BOUND('',#2722,.T.);
#2108=FACE_OUTER_BOUND('',#2723,.T.);
#2109=FACE_OUTER_BOUND('',#2724,.T.);
#2110=FACE_OUTER_BOUND('',#2725,.T.);
#2111=FACE_OUTER_BOUND('',#2726,.T.);
#2112=FACE_OUTER_BOUND('',#2727,.T.);
#2113=FACE_OUTER_BOUND('',#2728,.T.);
#2114=FACE_OUTER_BOUND('',#2729,.T.);
#2115=FACE_OUTER_BOUND('',#2730,.T.);
#2116=FACE_OUTER_BOUND('',#2731,.T.);
#2649=EDGE_LOOP('',(#6123,#6124,#6125,#6126,#6127,#6128));
#2650=EDGE_LOOP('',(#6129,#6130,#6131,#6132,#6133,#6134));
#2651=EDGE_LOOP('',(#6135,#6136,#6137,#6138));
#2652=EDGE_LOOP('',(#6139,#6140,#6141,#6142));
#2653=EDGE_LOOP('',(#6143,#6144,#6145,#6146));
#2654=EDGE_LOOP('',(#6147,#6148,#6149,#6150));
#2655=EDGE_LOOP('',(#6151,#6152,#6153,#6154));
#2656=EDGE_LOOP('',(#6155,#6156,#6157,#6158));
#2657=EDGE_LOOP('',(#6159,#6160,#6161,#6162));
#2658=EDGE_LOOP('',(#6163,#6164,#6165,#6166,#6167,#6168,#6169,#6170,#6171,
#6172,#6173,#6174,#6175,#6176,#6177,#6178,#6179,#6180,#6181,#6182,#6183,
#6184,#6185,#6186));
#2659=EDGE_LOOP('',(#6187,#6188,#6189,#6190,#6191,#6192));
#2660=EDGE_LOOP('',(#6193,#6194,#6195,#6196,#6197,#6198));
#2661=EDGE_LOOP('',(#6199,#6200,#6201,#6202));
#2662=EDGE_LOOP('',(#6203,#6204,#6205,#6206));
#2663=EDGE_LOOP('',(#6207,#6208,#6209,#6210,#6211,#6212,#6213,#6214,#6215,
#6216,#6217,#6218,#6219,#6220,#6221,#6222,#6223,#6224,#6225,#6226,#6227,
#6228,#6229,#6230));
#2664=EDGE_LOOP('',(#6231,#6232,#6233,#6234));
#2665=EDGE_LOOP('',(#6235,#6236,#6237,#6238));
#2666=EDGE_LOOP('',(#6239,#6240,#6241,#6242));
#2667=EDGE_LOOP('',(#6243,#6244,#6245,#6246));
#2668=EDGE_LOOP('',(#6247,#6248,#6249));
#2669=EDGE_LOOP('',(#6250,#6251,#6252));
#2670=EDGE_LOOP('',(#6253,#6254,#6255,#6256));
#2671=EDGE_LOOP('',(#6257,#6258,#6259));
#2672=EDGE_LOOP('',(#6260,#6261,#6262,#6263));
#2673=EDGE_LOOP('',(#6264,#6265,#6266,#6267));
#2674=EDGE_LOOP('',(#6268,#6269,#6270));
#2675=EDGE_LOOP('',(#6271,#6272,#6273,#6274));
#2676=EDGE_LOOP('',(#6275,#6276,#6277,#6278));
#2677=EDGE_LOOP('',(#6279,#6280,#6281,#6282));
#2678=EDGE_LOOP('',(#6283,#6284,#6285));
#2679=EDGE_LOOP('',(#6286,#6287,#6288,#6289));
#2680=EDGE_LOOP('',(#6290,#6291,#6292,#6293));
#2681=EDGE_LOOP('',(#6294,#6295,#6296,#6297));
#2682=EDGE_LOOP('',(#6298,#6299,#6300));
#2683=EDGE_LOOP('',(#6301,#6302,#6303,#6304));
#2684=EDGE_LOOP('',(#6305,#6306,#6307,#6308));
#2685=EDGE_LOOP('',(#6309,#6310,#6311,#6312));
#2686=EDGE_LOOP('',(#6313,#6314,#6315,#6316));
#2687=EDGE_LOOP('',(#6317,#6318,#6319));
#2688=EDGE_LOOP('',(#6320,#6321,#6322));
#2689=EDGE_LOOP('',(#6323,#6324,#6325,#6326));
#2690=EDGE_LOOP('',(#6327,#6328,#6329));
#2691=EDGE_LOOP('',(#6330,#6331,#6332,#6333));
#2692=EDGE_LOOP('',(#6334,#6335,#6336,#6337));
#2693=EDGE_LOOP('',(#6338,#6339,#6340));
#2694=EDGE_LOOP('',(#6341,#6342,#6343,#6344));
#2695=EDGE_LOOP('',(#6345,#6346,#6347,#6348));
#2696=EDGE_LOOP('',(#6349,#6350,#6351,#6352));
#2697=EDGE_LOOP('',(#6353,#6354,#6355));
#2698=EDGE_LOOP('',(#6356,#6357,#6358,#6359));
#2699=EDGE_LOOP('',(#6360,#6361,#6362,#6363));
#2700=EDGE_LOOP('',(#6364,#6365,#6366));
#2701=EDGE_LOOP('',(#6367,#6368,#6369,#6370));
#2702=EDGE_LOOP('',(#6371,#6372,#6373));
#2703=EDGE_LOOP('',(#6374,#6375,#6376,#6377));
#2704=EDGE_LOOP('',(#6378,#6379,#6380,#6381));
#2705=EDGE_LOOP('',(#6382,#6383,#6384));
#2706=EDGE_LOOP('',(#6385,#6386,#6387,#6388));
#2707=EDGE_LOOP('',(#6389,#6390,#6391,#6392));
#2708=EDGE_LOOP('',(#6393,#6394,#6395,#6396));
#2709=EDGE_LOOP('',(#6397,#6398,#6399,#6400));
#2710=EDGE_LOOP('',(#6401,#6402,#6403,#6404));
#2711=EDGE_LOOP('',(#6405,#6406,#6407,#6408));
#2712=EDGE_LOOP('',(#6409,#6410,#6411,#6412));
#2713=EDGE_LOOP('',(#6413,#6414,#6415,#6416));
#2714=EDGE_LOOP('',(#6417,#6418,#6419,#6420));
#2715=EDGE_LOOP('',(#6421,#6422,#6423,#6424));
#2716=EDGE_LOOP('',(#6425,#6426,#6427,#6428));
#2717=EDGE_LOOP('',(#6429,#6430,#6431,#6432));
#2718=EDGE_LOOP('',(#6433,#6434,#6435,#6436));
#2719=EDGE_LOOP('',(#6437,#6438,#6439,#6440));
#2720=EDGE_LOOP('',(#6441,#6442,#6443,#6444));
#2721=EDGE_LOOP('',(#6445,#6446,#6447,#6448));
#2722=EDGE_LOOP('',(#6449,#6450,#6451,#6452));
#2723=EDGE_LOOP('',(#6453,#6454,#6455,#6456));
#2724=EDGE_LOOP('',(#6457,#6458,#6459,#6460));
#2725=EDGE_LOOP('',(#6461,#6462,#6463,#6464));
#2726=EDGE_LOOP('',(#6465,#6466,#6467,#6468));
#2727=EDGE_LOOP('',(#6469,#6470,#6471,#6472));
#2728=EDGE_LOOP('',(#6473,#6474,#6475,#6476));
#2729=EDGE_LOOP('',(#6477,#6478,#6479,#6480));
#2730=EDGE_LOOP('',(#6481,#6482,#6483,#6484));
#2731=EDGE_LOOP('',(#6485,#6486,#6487,#6488));
#3314=CIRCLE('',#9766,0.5);
#3315=CIRCLE('',#9767,0.5);
#3316=CIRCLE('',#9769,0.5);
#3317=CIRCLE('',#9770,0.5);
#3318=CIRCLE('',#9775,0.500000000000007);
#3319=CIRCLE('',#9781,0.500000000000007);
#3320=CIRCLE('',#9783,0.999999999999972);
#3321=CIRCLE('',#9784,1.);
#3322=CIRCLE('',#9785,0.999999999999997);
#3323=CIRCLE('',#9786,0.999999999999996);
#3324=CIRCLE('',#9788,0.5);
#3325=CIRCLE('',#9789,0.5);
#3326=CIRCLE('',#9791,0.5);
#3327=CIRCLE('',#9792,0.5);
#3328=CIRCLE('',#9795,0.500000000000007);
#3329=CIRCLE('',#9797,1.);
#3330=CIRCLE('',#9798,1.);
#3331=CIRCLE('',#9799,1.);
#3332=CIRCLE('',#9800,0.999999999999992);
#3333=CIRCLE('',#9803,0.500000000000007);
#3334=CIRCLE('',#9805,0.5);
#3335=CIRCLE('',#9806,0.499999999999998);
#3336=CIRCLE('',#9807,0.500000000000007);
#3337=CIRCLE('',#9809,0.500000000000007);
#3338=CIRCLE('',#9810,0.5);
#3339=CIRCLE('',#9811,0.500000000000007);
#3340=CIRCLE('',#9813,0.500000000000007);
#3341=CIRCLE('',#9814,0.499999999999998);
#3342=CIRCLE('',#9815,0.5);
#3343=CIRCLE('',#9817,0.500000000000007);
#3344=CIRCLE('',#9818,0.499999999999998);
#3345=CIRCLE('',#9819,0.499999999999998);
#3346=CIRCLE('',#9822,0.500000000000007);
#3347=CIRCLE('',#9823,0.5);
#3348=CIRCLE('',#9824,0.499999999999998);
#3349=CIRCLE('',#9828,0.5);
#3350=CIRCLE('',#9829,0.499999999999998);
#3351=CIRCLE('',#9830,0.500000000000007);
#3352=CIRCLE('',#9834,0.5);
#3353=CIRCLE('',#9835,0.499999999999998);
#3354=CIRCLE('',#9836,0.500000000000007);
#3355=CIRCLE('',#9838,0.499999999999998);
#3356=CIRCLE('',#9839,0.5);
#3357=CIRCLE('',#9841,0.499999999999998);
#3358=CIRCLE('',#9842,0.5);
#3359=CIRCLE('',#9843,0.500000000000007);
#3360=CIRCLE('',#9847,0.500000000000007);
#3361=CIRCLE('',#9848,0.5);
#3362=CIRCLE('',#9850,0.500000000000005);
#3363=CIRCLE('',#9851,0.5);
#3364=CIRCLE('',#9852,0.500000000000007);
#3365=CIRCLE('',#9854,0.5);
#3366=CIRCLE('',#9855,0.5);
#3367=CIRCLE('',#9856,0.500000000000007);
#3368=CIRCLE('',#9860,0.500000000000007);
#3369=CIRCLE('',#9861,0.5);
#3370=CIRCLE('',#9862,0.499999999999998);
#3371=CIRCLE('',#9864,0.500000000000007);
#3372=CIRCLE('',#9865,0.5);
#3373=CIRCLE('',#9866,0.499999999999998);
#3374=CIRCLE('',#9869,0.500000000000007);
#3375=CIRCLE('',#9870,0.5);
#3376=CIRCLE('',#9871,0.5);
#3377=CIRCLE('',#9875,0.5);
#3378=CIRCLE('',#9876,0.500000000000007);
#3379=CIRCLE('',#9880,0.499999999999999);
#3380=CIRCLE('',#9881,0.499999999999998);
#3381=CIRCLE('',#9882,0.500000000000007);
#3382=CIRCLE('',#9884,0.500000000000007);
#3383=CIRCLE('',#9885,0.5);
#3384=CIRCLE('',#9888,0.5);
#3385=CIRCLE('',#9889,0.499999999999999);
#3386=CIRCLE('',#9890,0.500000000000007);
#3387=CIRCLE('',#9892,0.499999999999998);
#3388=CIRCLE('',#9893,0.500000000000007);
#3389=CIRCLE('',#9894,0.5);
#3390=CIRCLE('',#9897,0.499999999999999);
#3391=CIRCLE('',#9898,0.500000000000007);
#3392=CIRCLE('',#9899,0.5);
#3393=CIRCLE('',#9903,0.499999999999999);
#3394=CIRCLE('',#9904,0.499999999999998);
#3395=CIRCLE('',#9905,0.500000000000007);
#3942=VERTEX_POINT('',#14290);
#3943=VERTEX_POINT('',#14291);
#3944=VERTEX_POINT('',#14293);
#3945=VERTEX_POINT('',#14295);
#3946=VERTEX_POINT('',#14297);
#3947=VERTEX_POINT('',#14299);
#3948=VERTEX_POINT('',#14303);
#3949=VERTEX_POINT('',#14304);
#3950=VERTEX_POINT('',#14306);
#3951=VERTEX_POINT('',#14308);
#3952=VERTEX_POINT('',#14310);
#3953=VERTEX_POINT('',#14312);
#3954=VERTEX_POINT('',#14319);
#3955=VERTEX_POINT('',#14321);
#3956=VERTEX_POINT('',#14325);
#3957=VERTEX_POINT('',#14327);
#3958=VERTEX_POINT('',#14331);
#3959=VERTEX_POINT('',#14335);
#3960=VERTEX_POINT('',#14339);
#3961=VERTEX_POINT('',#14343);
#3962=VERTEX_POINT('',#14347);
#3963=VERTEX_POINT('',#14349);
#3964=VERTEX_POINT('',#14351);
#3965=VERTEX_POINT('',#14353);
#3966=VERTEX_POINT('',#14355);
#3967=VERTEX_POINT('',#14357);
#3968=VERTEX_POINT('',#14359);
#3969=VERTEX_POINT('',#14361);
#3970=VERTEX_POINT('',#14363);
#3971=VERTEX_POINT('',#14365);
#3972=VERTEX_POINT('',#14367);
#3973=VERTEX_POINT('',#14369);
#3974=VERTEX_POINT('',#14371);
#3975=VERTEX_POINT('',#14373);
#3976=VERTEX_POINT('',#14375);
#3977=VERTEX_POINT('',#14377);
#3978=VERTEX_POINT('',#14379);
#3979=VERTEX_POINT('',#14381);
#3980=VERTEX_POINT('',#14385);
#3981=VERTEX_POINT('',#14387);
#3982=VERTEX_POINT('',#14389);
#3983=VERTEX_POINT('',#14391);
#3984=VERTEX_POINT('',#14395);
#3985=VERTEX_POINT('',#14397);
#3986=VERTEX_POINT('',#14399);
#3987=VERTEX_POINT('',#14401);
#3988=VERTEX_POINT('',#14407);
#3989=VERTEX_POINT('',#14411);
#3990=VERTEX_POINT('',#14413);
#3991=VERTEX_POINT('',#14415);
#3992=VERTEX_POINT('',#14417);
#3993=VERTEX_POINT('',#14419);
#3994=VERTEX_POINT('',#14421);
#3995=VERTEX_POINT('',#14423);
#3996=VERTEX_POINT('',#14425);
#3997=VERTEX_POINT('',#14427);
#3998=VERTEX_POINT('',#14429);
#3999=VERTEX_POINT('',#14431);
#4000=VERTEX_POINT('',#14433);
#4001=VERTEX_POINT('',#14435);
#4002=VERTEX_POINT('',#14438);
#4003=VERTEX_POINT('',#14442);
#4004=VERTEX_POINT('',#14446);
#4005=VERTEX_POINT('',#14450);
#4006=VERTEX_POINT('',#14452);
#4007=VERTEX_POINT('',#14456);
#4008=VERTEX_POINT('',#14458);
#4009=VERTEX_POINT('',#14462);
#4010=VERTEX_POINT('',#14464);
#4011=VERTEX_POINT('',#14468);
#4012=VERTEX_POINT('',#14470);
#4013=VERTEX_POINT('',#14476);
#4014=VERTEX_POINT('',#14478);
#4015=VERTEX_POINT('',#14487);
#4016=VERTEX_POINT('',#14489);
#4017=VERTEX_POINT('',#14498);
#4018=VERTEX_POINT('',#14500);
#4019=VERTEX_POINT('',#14504);
#4020=VERTEX_POINT('',#14508);
#4021=VERTEX_POINT('',#14510);
#4022=VERTEX_POINT('',#14519);
#4023=VERTEX_POINT('',#14523);
#4024=VERTEX_POINT('',#14525);
#4025=VERTEX_POINT('',#14529);
#4026=VERTEX_POINT('',#14531);
#4027=VERTEX_POINT('',#14540);
#4028=VERTEX_POINT('',#14542);
#4029=VERTEX_POINT('',#14546);
#4030=VERTEX_POINT('',#14548);
#4031=VERTEX_POINT('',#14554);
#4032=VERTEX_POINT('',#14556);
#4033=VERTEX_POINT('',#14565);
#4034=VERTEX_POINT('',#14574);
#4035=VERTEX_POINT('',#14576);
#4036=VERTEX_POINT('',#14580);
#4037=VERTEX_POINT('',#14586);
#4038=VERTEX_POINT('',#14588);
#4039=VERTEX_POINT('',#14592);
#4040=VERTEX_POINT('',#14598);
#4041=VERTEX_POINT('',#14599);
#4042=VERTEX_POINT('',#14608);
#4043=VERTEX_POINT('',#14610);
#4732=EDGE_CURVE('',#3942,#3943,#3314,.T.);
#4733=EDGE_CURVE('',#3944,#3942,#644,.T.);
#4734=EDGE_CURVE('',#3944,#3945,#645,.T.);
#4735=EDGE_CURVE('',#3946,#3945,#646,.T.);
#4736=EDGE_CURVE('',#3947,#3946,#3315,.T.);
#4737=EDGE_CURVE('',#3943,#3947,#647,.T.);
#4738=EDGE_CURVE('',#3948,#3949,#3316,.T.);
#4739=EDGE_CURVE('',#3950,#3948,#648,.T.);
#4740=EDGE_CURVE('',#3951,#3950,#3317,.T.);
#4741=EDGE_CURVE('',#3952,#3951,#649,.T.);
#4742=EDGE_CURVE('',#3953,#3952,#650,.T.);
#4743=EDGE_CURVE('',#3949,#3953,#651,.T.);
#4744=EDGE_CURVE('',#3945,#3952,#652,.T.);
#4745=EDGE_CURVE('',#3953,#3944,#653,.T.);
#4746=EDGE_CURVE('',#3949,#3954,#654,.T.);
#4747=EDGE_CURVE('',#3954,#3955,#267,.T.);
#4748=EDGE_CURVE('',#3955,#3948,#655,.T.);
#4749=EDGE_CURVE('',#3943,#3956,#656,.T.);
#4750=EDGE_CURVE('',#3956,#3957,#3318,.F.);
#4751=EDGE_CURVE('',#3957,#3942,#657,.T.);
#4752=EDGE_CURVE('',#3955,#3958,#658,.T.);
#4753=EDGE_CURVE('',#3950,#3958,#659,.T.);
#4754=EDGE_CURVE('',#3959,#3947,#660,.T.);
#4755=EDGE_CURVE('',#3956,#3959,#661,.T.);
#4756=EDGE_CURVE('',#3960,#3958,#268,.T.);
#4757=EDGE_CURVE('',#3960,#3951,#662,.T.);
#4758=EDGE_CURVE('',#3946,#3961,#663,.T.);
#4759=EDGE_CURVE('',#3961,#3959,#3319,.F.);
#4760=EDGE_CURVE('',#3962,#3960,#664,.T.);
#4761=EDGE_CURVE('',#3963,#3962,#665,.T.);
#4762=EDGE_CURVE('',#3963,#3964,#666,.T.);
#4763=EDGE_CURVE('',#3964,#3965,#667,.T.);
#4764=EDGE_CURVE('',#3965,#3966,#668,.T.);
#4765=EDGE_CURVE('',#3967,#3966,#669,.T.);
#4766=EDGE_CURVE('',#3968,#3967,#670,.T.);
#4767=EDGE_CURVE('',#3969,#3968,#671,.T.);
#4768=EDGE_CURVE('',#3970,#3969,#3320,.T.);
#4769=EDGE_CURVE('',#3971,#3970,#672,.T.);
#4770=EDGE_CURVE('',#3972,#3971,#673,.T.);
#4771=EDGE_CURVE('',#3973,#3972,#3321,.T.);
#4772=EDGE_CURVE('',#3974,#3973,#674,.T.);
#4773=EDGE_CURVE('',#3975,#3974,#3322,.T.);
#4774=EDGE_CURVE('',#3976,#3975,#675,.T.);
#4775=EDGE_CURVE('',#3977,#3976,#676,.T.);
#4776=EDGE_CURVE('',#3978,#3977,#3323,.T.);
#4777=EDGE_CURVE('',#3979,#3978,#677,.T.);
#4778=EDGE_CURVE('',#3961,#3979,#678,.T.);
#4779=EDGE_CURVE('',#3966,#3980,#3324,.T.);
#4780=EDGE_CURVE('',#3981,#3965,#679,.T.);
#4781=EDGE_CURVE('',#3982,#3981,#680,.T.);
#4782=EDGE_CURVE('',#3983,#3982,#3325,.T.);
#4783=EDGE_CURVE('',#3980,#3983,#681,.T.);
#4784=EDGE_CURVE('',#3984,#3963,#3326,.T.);
#4785=EDGE_CURVE('',#3985,#3984,#682,.T.);
#4786=EDGE_CURVE('',#3986,#3985,#3327,.T.);
#4787=EDGE_CURVE('',#3987,#3986,#683,.T.);
#4788=EDGE_CURVE('',#3987,#3964,#684,.T.);
#4789=EDGE_CURVE('',#3981,#3987,#685,.T.);
#4790=EDGE_CURVE('',#3980,#3988,#686,.T.);
#4791=EDGE_CURVE('',#3988,#3967,#3328,.F.);
#4792=EDGE_CURVE('',#3989,#3957,#687,.T.);
#4793=EDGE_CURVE('',#3990,#3989,#688,.T.);
#4794=EDGE_CURVE('',#3991,#3990,#3329,.T.);
#4795=EDGE_CURVE('',#3992,#3991,#689,.T.);
#4796=EDGE_CURVE('',#3993,#3992,#690,.T.);
#4797=EDGE_CURVE('',#3994,#3993,#3330,.T.);
#4798=EDGE_CURVE('',#3995,#3994,#691,.T.);
#4799=EDGE_CURVE('',#3996,#3995,#3331,.T.);
#4800=EDGE_CURVE('',#3997,#3996,#692,.T.);
#4801=EDGE_CURVE('',#3998,#3997,#693,.T.);
#4802=EDGE_CURVE('',#3999,#3998,#3332,.T.);
#4803=EDGE_CURVE('',#4000,#3999,#694,.T.);
#4804=EDGE_CURVE('',#4001,#4000,#695,.T.);
#4805=EDGE_CURVE('',#3982,#4001,#696,.T.);
#4806=EDGE_CURVE('',#4002,#3986,#697,.T.);
#4807=EDGE_CURVE('',#3954,#4002,#698,.T.);
#4808=EDGE_CURVE('',#4003,#3983,#699,.T.);
#4809=EDGE_CURVE('',#3988,#4003,#700,.T.);
#4810=EDGE_CURVE('',#3985,#4004,#701,.T.);
#4811=EDGE_CURVE('',#4004,#4002,#3333,.F.);
#4812=EDGE_CURVE('',#4005,#3977,#3334,.T.);
#4813=EDGE_CURVE('',#4006,#4005,#3335,.F.);
#4814=EDGE_CURVE('',#3978,#4006,#3336,.T.);
#4815=EDGE_CURVE('',#4007,#3990,#3337,.T.);
#4816=EDGE_CURVE('',#4008,#4007,#3338,.F.);
#4817=EDGE_CURVE('',#3991,#4008,#3339,.T.);
#4818=EDGE_CURVE('',#3976,#4009,#3340,.F.);
#4819=EDGE_CURVE('',#4010,#3976,#3341,.F.);
#4820=EDGE_CURVE('',#4009,#4010,#3342,.F.);
#4821=EDGE_CURVE('',#3979,#4011,#3343,.F.);
#4822=EDGE_CURVE('',#4012,#3979,#3344,.F.);
#4823=EDGE_CURVE('',#4011,#4012,#3345,.F.);
#4824=EDGE_CURVE('',#4006,#4012,#702,.T.);
#4825=EDGE_CURVE('',#3992,#4013,#3346,.F.);
#4826=EDGE_CURVE('',#4014,#3992,#3347,.F.);
#4827=EDGE_CURVE('',#4013,#4014,#3348,.F.);
#4828=EDGE_CURVE('',#4008,#4014,#703,.T.);
#4829=EDGE_CURVE('',#4014,#4009,#704,.T.);
#4830=EDGE_CURVE('',#4010,#4013,#705,.T.);
#4831=EDGE_CURVE('',#4015,#3989,#3349,.F.);
#4832=EDGE_CURVE('',#4016,#4015,#3350,.F.);
#4833=EDGE_CURVE('',#3989,#4016,#3351,.F.);
#4834=EDGE_CURVE('',#4015,#4011,#706,.T.);
#4835=EDGE_CURVE('',#4012,#4016,#707,.T.);
#4836=EDGE_CURVE('',#4016,#4007,#708,.T.);
#4837=EDGE_CURVE('',#4017,#3974,#3352,.T.);
#4838=EDGE_CURVE('',#4018,#4017,#3353,.F.);
#4839=EDGE_CURVE('',#3975,#4018,#3354,.T.);
#4840=EDGE_CURVE('',#3959,#4019,#3355,.F.);
#4841=EDGE_CURVE('',#4019,#3961,#3356,.F.);
#4842=EDGE_CURVE('',#4020,#3993,#3357,.T.);
#4843=EDGE_CURVE('',#4021,#4020,#3358,.F.);
#4844=EDGE_CURVE('',#3994,#4021,#3359,.T.);
#4845=EDGE_CURVE('',#4013,#4020,#709,.T.);
#4846=EDGE_CURVE('',#4020,#4018,#710,.T.);
#4847=EDGE_CURVE('',#4017,#4021,#711,.T.);
#4848=EDGE_CURVE('',#3957,#4022,#3360,.F.);
#4849=EDGE_CURVE('',#4022,#3956,#3361,.F.);
#4850=EDGE_CURVE('',#4023,#3972,#3362,.T.);
#4851=EDGE_CURVE('',#4024,#4023,#3363,.F.);
#4852=EDGE_CURVE('',#3973,#4024,#3364,.T.);
#4853=EDGE_CURVE('',#4025,#3995,#3365,.T.);
#4854=EDGE_CURVE('',#4026,#4025,#3366,.F.);
#4855=EDGE_CURVE('',#3996,#4026,#3367,.T.);
#4856=EDGE_CURVE('',#4021,#4025,#712,.T.);
#4857=EDGE_CURVE('',#4025,#4024,#713,.T.);
#4858=EDGE_CURVE('',#4023,#4026,#714,.T.);
#4859=EDGE_CURVE('',#3971,#4027,#3368,.F.);
#4860=EDGE_CURVE('',#4028,#3971,#3369,.F.);
#4861=EDGE_CURVE('',#4027,#4028,#3370,.F.);
#4862=EDGE_CURVE('',#3962,#4029,#3371,.F.);
#4863=EDGE_CURVE('',#4030,#3962,#3372,.F.);
#4864=EDGE_CURVE('',#4029,#4030,#3373,.F.);
#4865=EDGE_CURVE('',#3958,#4030,#715,.T.);
#4866=EDGE_CURVE('',#3997,#4031,#3374,.F.);
#4867=EDGE_CURVE('',#4032,#3997,#3375,.F.);
#4868=EDGE_CURVE('',#4031,#4032,#3376,.F.);
#4869=EDGE_CURVE('',#4026,#4032,#716,.T.);
#4870=EDGE_CURVE('',#4032,#4027,#717,.T.);
#4871=EDGE_CURVE('',#4028,#4031,#718,.T.);
#4872=EDGE_CURVE('',#4033,#4004,#3377,.F.);
#4873=EDGE_CURVE('',#4002,#4033,#3378,.F.);
#4874=EDGE_CURVE('',#4004,#4029,#719,.T.);
#4875=EDGE_CURVE('',#4030,#4033,#720,.T.);
#4876=EDGE_CURVE('',#4033,#3955,#721,.T.);
#4877=EDGE_CURVE('',#4034,#3969,#3379,.T.);
#4878=EDGE_CURVE('',#4035,#4034,#3380,.F.);
#4879=EDGE_CURVE('',#3970,#4035,#3381,.T.);
#4880=EDGE_CURVE('',#3967,#4036,#3382,.F.);
#4881=EDGE_CURVE('',#4036,#3988,#3383,.F.);
#4882=EDGE_CURVE('',#4029,#3984,#722,.T.);
#4883=EDGE_CURVE('',#4037,#3998,#3384,.T.);
#4884=EDGE_CURVE('',#4038,#4037,#3385,.F.);
#4885=EDGE_CURVE('',#3999,#4038,#3386,.T.);
#4886=EDGE_CURVE('',#4003,#4039,#3387,.F.);
#4887=EDGE_CURVE('',#4001,#4003,#3388,.F.);
#4888=EDGE_CURVE('',#4039,#4001,#3389,.F.);
#4889=EDGE_CURVE('',#4040,#4041,#3390,.F.);
#4890=EDGE_CURVE('',#3968,#4040,#3391,.F.);
#4891=EDGE_CURVE('',#4041,#3968,#3392,.F.);
#4892=EDGE_CURVE('',#4040,#4034,#723,.T.);
#4893=EDGE_CURVE('',#4036,#4041,#724,.T.);
#4894=EDGE_CURVE('',#4042,#4000,#3393,.F.);
#4895=EDGE_CURVE('',#4043,#4042,#3394,.F.);
#4896=EDGE_CURVE('',#4000,#4043,#3395,.F.);
#4897=EDGE_CURVE('',#4041,#4043,#725,.T.);
#4898=EDGE_CURVE('',#4042,#4040,#726,.T.);
#4899=EDGE_CURVE('',#4043,#4039,#727,.T.);
#4900=EDGE_CURVE('',#4038,#4042,#728,.T.);
#4901=EDGE_CURVE('',#4039,#4036,#729,.T.);
#4902=EDGE_CURVE('',#4031,#4037,#730,.T.);
#4903=EDGE_CURVE('',#4037,#4035,#731,.T.);
#4904=EDGE_CURVE('',#4034,#4038,#732,.T.);
#4905=EDGE_CURVE('',#4035,#4028,#733,.T.);
#4906=EDGE_CURVE('',#4027,#4023,#734,.T.);
#4907=EDGE_CURVE('',#4024,#4017,#735,.T.);
#4908=EDGE_CURVE('',#4019,#4022,#736,.T.);
#4909=EDGE_CURVE('',#4022,#4015,#737,.T.);
#4910=EDGE_CURVE('',#4011,#4019,#738,.T.);
#4911=EDGE_CURVE('',#4018,#4010,#739,.T.);
#4912=EDGE_CURVE('',#4009,#4005,#740,.T.);
#4913=EDGE_CURVE('',#4007,#4006,#741,.T.);
#4914=EDGE_CURVE('',#4005,#4008,#742,.T.);
#6123=ORIENTED_EDGE('',*,*,#4732,.F.);
#6124=ORIENTED_EDGE('',*,*,#4733,.F.);
#6125=ORIENTED_EDGE('',*,*,#4734,.T.);
#6126=ORIENTED_EDGE('',*,*,#4735,.F.);
#6127=ORIENTED_EDGE('',*,*,#4736,.F.);
#6128=ORIENTED_EDGE('',*,*,#4737,.F.);
#6129=ORIENTED_EDGE('',*,*,#4738,.F.);
#6130=ORIENTED_EDGE('',*,*,#4739,.F.);
#6131=ORIENTED_EDGE('',*,*,#4740,.F.);
#6132=ORIENTED_EDGE('',*,*,#4741,.F.);
#6133=ORIENTED_EDGE('',*,*,#4742,.F.);
#6134=ORIENTED_EDGE('',*,*,#4743,.F.);
#6135=ORIENTED_EDGE('',*,*,#4742,.T.);
#6136=ORIENTED_EDGE('',*,*,#4744,.F.);
#6137=ORIENTED_EDGE('',*,*,#4734,.F.);
#6138=ORIENTED_EDGE('',*,*,#4745,.F.);
#6139=ORIENTED_EDGE('',*,*,#4738,.T.);
#6140=ORIENTED_EDGE('',*,*,#4746,.T.);
#6141=ORIENTED_EDGE('',*,*,#4747,.T.);
#6142=ORIENTED_EDGE('',*,*,#4748,.T.);
#6143=ORIENTED_EDGE('',*,*,#4732,.T.);
#6144=ORIENTED_EDGE('',*,*,#4749,.T.);
#6145=ORIENTED_EDGE('',*,*,#4750,.T.);
#6146=ORIENTED_EDGE('',*,*,#4751,.T.);
#6147=ORIENTED_EDGE('',*,*,#4739,.T.);
#6148=ORIENTED_EDGE('',*,*,#4748,.F.);
#6149=ORIENTED_EDGE('',*,*,#4752,.T.);
#6150=ORIENTED_EDGE('',*,*,#4753,.F.);
#6151=ORIENTED_EDGE('',*,*,#4737,.T.);
#6152=ORIENTED_EDGE('',*,*,#4754,.F.);
#6153=ORIENTED_EDGE('',*,*,#4755,.F.);
#6154=ORIENTED_EDGE('',*,*,#4749,.F.);
#6155=ORIENTED_EDGE('',*,*,#4740,.T.);
#6156=ORIENTED_EDGE('',*,*,#4753,.T.);
#6157=ORIENTED_EDGE('',*,*,#4756,.F.);
#6158=ORIENTED_EDGE('',*,*,#4757,.T.);
#6159=ORIENTED_EDGE('',*,*,#4736,.T.);
#6160=ORIENTED_EDGE('',*,*,#4758,.T.);
#6161=ORIENTED_EDGE('',*,*,#4759,.T.);
#6162=ORIENTED_EDGE('',*,*,#4754,.T.);
#6163=ORIENTED_EDGE('',*,*,#4735,.T.);
#6164=ORIENTED_EDGE('',*,*,#4744,.T.);
#6165=ORIENTED_EDGE('',*,*,#4741,.T.);
#6166=ORIENTED_EDGE('',*,*,#4757,.F.);
#6167=ORIENTED_EDGE('',*,*,#4760,.F.);
#6168=ORIENTED_EDGE('',*,*,#4761,.F.);
#6169=ORIENTED_EDGE('',*,*,#4762,.T.);
#6170=ORIENTED_EDGE('',*,*,#4763,.T.);
#6171=ORIENTED_EDGE('',*,*,#4764,.T.);
#6172=ORIENTED_EDGE('',*,*,#4765,.F.);
#6173=ORIENTED_EDGE('',*,*,#4766,.F.);
#6174=ORIENTED_EDGE('',*,*,#4767,.F.);
#6175=ORIENTED_EDGE('',*,*,#4768,.F.);
#6176=ORIENTED_EDGE('',*,*,#4769,.F.);
#6177=ORIENTED_EDGE('',*,*,#4770,.F.);
#6178=ORIENTED_EDGE('',*,*,#4771,.F.);
#6179=ORIENTED_EDGE('',*,*,#4772,.F.);
#6180=ORIENTED_EDGE('',*,*,#4773,.F.);
#6181=ORIENTED_EDGE('',*,*,#4774,.F.);
#6182=ORIENTED_EDGE('',*,*,#4775,.F.);
#6183=ORIENTED_EDGE('',*,*,#4776,.F.);
#6184=ORIENTED_EDGE('',*,*,#4777,.F.);
#6185=ORIENTED_EDGE('',*,*,#4778,.F.);
#6186=ORIENTED_EDGE('',*,*,#4758,.F.);
#6187=ORIENTED_EDGE('',*,*,#4779,.F.);
#6188=ORIENTED_EDGE('',*,*,#4764,.F.);
#6189=ORIENTED_EDGE('',*,*,#4780,.F.);
#6190=ORIENTED_EDGE('',*,*,#4781,.F.);
#6191=ORIENTED_EDGE('',*,*,#4782,.F.);
#6192=ORIENTED_EDGE('',*,*,#4783,.F.);
#6193=ORIENTED_EDGE('',*,*,#4784,.F.);
#6194=ORIENTED_EDGE('',*,*,#4785,.F.);
#6195=ORIENTED_EDGE('',*,*,#4786,.F.);
#6196=ORIENTED_EDGE('',*,*,#4787,.F.);
#6197=ORIENTED_EDGE('',*,*,#4788,.T.);
#6198=ORIENTED_EDGE('',*,*,#4762,.F.);
#6199=ORIENTED_EDGE('',*,*,#4788,.F.);
#6200=ORIENTED_EDGE('',*,*,#4789,.F.);
#6201=ORIENTED_EDGE('',*,*,#4780,.T.);
#6202=ORIENTED_EDGE('',*,*,#4763,.F.);
#6203=ORIENTED_EDGE('',*,*,#4779,.T.);
#6204=ORIENTED_EDGE('',*,*,#4790,.T.);
#6205=ORIENTED_EDGE('',*,*,#4791,.T.);
#6206=ORIENTED_EDGE('',*,*,#4765,.T.);
#6207=ORIENTED_EDGE('',*,*,#4733,.T.);
#6208=ORIENTED_EDGE('',*,*,#4751,.F.);
#6209=ORIENTED_EDGE('',*,*,#4792,.F.);
#6210=ORIENTED_EDGE('',*,*,#4793,.F.);
#6211=ORIENTED_EDGE('',*,*,#4794,.F.);
#6212=ORIENTED_EDGE('',*,*,#4795,.F.);
#6213=ORIENTED_EDGE('',*,*,#4796,.F.);
#6214=ORIENTED_EDGE('',*,*,#4797,.F.);
#6215=ORIENTED_EDGE('',*,*,#4798,.F.);
#6216=ORIENTED_EDGE('',*,*,#4799,.F.);
#6217=ORIENTED_EDGE('',*,*,#4800,.F.);
#6218=ORIENTED_EDGE('',*,*,#4801,.F.);
#6219=ORIENTED_EDGE('',*,*,#4802,.F.);
#6220=ORIENTED_EDGE('',*,*,#4803,.F.);
#6221=ORIENTED_EDGE('',*,*,#4804,.F.);
#6222=ORIENTED_EDGE('',*,*,#4805,.F.);
#6223=ORIENTED_EDGE('',*,*,#4781,.T.);
#6224=ORIENTED_EDGE('',*,*,#4789,.T.);
#6225=ORIENTED_EDGE('',*,*,#4787,.T.);
#6226=ORIENTED_EDGE('',*,*,#4806,.F.);
#6227=ORIENTED_EDGE('',*,*,#4807,.F.);
#6228=ORIENTED_EDGE('',*,*,#4746,.F.);
#6229=ORIENTED_EDGE('',*,*,#4743,.T.);
#6230=ORIENTED_EDGE('',*,*,#4745,.T.);
#6231=ORIENTED_EDGE('',*,*,#4783,.T.);
#6232=ORIENTED_EDGE('',*,*,#4808,.F.);
#6233=ORIENTED_EDGE('',*,*,#4809,.F.);
#6234=ORIENTED_EDGE('',*,*,#4790,.F.);
#6235=ORIENTED_EDGE('',*,*,#4786,.T.);
#6236=ORIENTED_EDGE('',*,*,#4810,.T.);
#6237=ORIENTED_EDGE('',*,*,#4811,.T.);
#6238=ORIENTED_EDGE('',*,*,#4806,.T.);
#6239=ORIENTED_EDGE('',*,*,#4776,.T.);
#6240=ORIENTED_EDGE('',*,*,#4812,.F.);
#6241=ORIENTED_EDGE('',*,*,#4813,.F.);
#6242=ORIENTED_EDGE('',*,*,#4814,.F.);
#6243=ORIENTED_EDGE('',*,*,#4794,.T.);
#6244=ORIENTED_EDGE('',*,*,#4815,.F.);
#6245=ORIENTED_EDGE('',*,*,#4816,.F.);
#6246=ORIENTED_EDGE('',*,*,#4817,.F.);
#6247=ORIENTED_EDGE('',*,*,#4818,.F.);
#6248=ORIENTED_EDGE('',*,*,#4819,.F.);
#6249=ORIENTED_EDGE('',*,*,#4820,.F.);
#6250=ORIENTED_EDGE('',*,*,#4821,.F.);
#6251=ORIENTED_EDGE('',*,*,#4822,.F.);
#6252=ORIENTED_EDGE('',*,*,#4823,.F.);
#6253=ORIENTED_EDGE('',*,*,#4822,.T.);
#6254=ORIENTED_EDGE('',*,*,#4777,.T.);
#6255=ORIENTED_EDGE('',*,*,#4814,.T.);
#6256=ORIENTED_EDGE('',*,*,#4824,.T.);
#6257=ORIENTED_EDGE('',*,*,#4825,.F.);
#6258=ORIENTED_EDGE('',*,*,#4826,.F.);
#6259=ORIENTED_EDGE('',*,*,#4827,.F.);
#6260=ORIENTED_EDGE('',*,*,#4826,.T.);
#6261=ORIENTED_EDGE('',*,*,#4795,.T.);
#6262=ORIENTED_EDGE('',*,*,#4817,.T.);
#6263=ORIENTED_EDGE('',*,*,#4828,.T.);
#6264=ORIENTED_EDGE('',*,*,#4827,.T.);
#6265=ORIENTED_EDGE('',*,*,#4829,.T.);
#6266=ORIENTED_EDGE('',*,*,#4820,.T.);
#6267=ORIENTED_EDGE('',*,*,#4830,.T.);
#6268=ORIENTED_EDGE('',*,*,#4831,.F.);
#6269=ORIENTED_EDGE('',*,*,#4832,.F.);
#6270=ORIENTED_EDGE('',*,*,#4833,.F.);
#6271=ORIENTED_EDGE('',*,*,#4832,.T.);
#6272=ORIENTED_EDGE('',*,*,#4834,.T.);
#6273=ORIENTED_EDGE('',*,*,#4823,.T.);
#6274=ORIENTED_EDGE('',*,*,#4835,.T.);
#6275=ORIENTED_EDGE('',*,*,#4815,.T.);
#6276=ORIENTED_EDGE('',*,*,#4793,.T.);
#6277=ORIENTED_EDGE('',*,*,#4833,.T.);
#6278=ORIENTED_EDGE('',*,*,#4836,.T.);
#6279=ORIENTED_EDGE('',*,*,#4773,.T.);
#6280=ORIENTED_EDGE('',*,*,#4837,.F.);
#6281=ORIENTED_EDGE('',*,*,#4838,.F.);
#6282=ORIENTED_EDGE('',*,*,#4839,.F.);
#6283=ORIENTED_EDGE('',*,*,#4840,.F.);
#6284=ORIENTED_EDGE('',*,*,#4759,.F.);
#6285=ORIENTED_EDGE('',*,*,#4841,.F.);
#6286=ORIENTED_EDGE('',*,*,#4797,.T.);
#6287=ORIENTED_EDGE('',*,*,#4842,.F.);
#6288=ORIENTED_EDGE('',*,*,#4843,.F.);
#6289=ORIENTED_EDGE('',*,*,#4844,.F.);
#6290=ORIENTED_EDGE('',*,*,#4842,.T.);
#6291=ORIENTED_EDGE('',*,*,#4796,.T.);
#6292=ORIENTED_EDGE('',*,*,#4825,.T.);
#6293=ORIENTED_EDGE('',*,*,#4845,.T.);
#6294=ORIENTED_EDGE('',*,*,#4843,.T.);
#6295=ORIENTED_EDGE('',*,*,#4846,.T.);
#6296=ORIENTED_EDGE('',*,*,#4838,.T.);
#6297=ORIENTED_EDGE('',*,*,#4847,.T.);
#6298=ORIENTED_EDGE('',*,*,#4848,.F.);
#6299=ORIENTED_EDGE('',*,*,#4750,.F.);
#6300=ORIENTED_EDGE('',*,*,#4849,.F.);
#6301=ORIENTED_EDGE('',*,*,#4771,.T.);
#6302=ORIENTED_EDGE('',*,*,#4850,.F.);
#6303=ORIENTED_EDGE('',*,*,#4851,.F.);
#6304=ORIENTED_EDGE('',*,*,#4852,.F.);
#6305=ORIENTED_EDGE('',*,*,#4799,.T.);
#6306=ORIENTED_EDGE('',*,*,#4853,.F.);
#6307=ORIENTED_EDGE('',*,*,#4854,.F.);
#6308=ORIENTED_EDGE('',*,*,#4855,.F.);
#6309=ORIENTED_EDGE('',*,*,#4853,.T.);
#6310=ORIENTED_EDGE('',*,*,#4798,.T.);
#6311=ORIENTED_EDGE('',*,*,#4844,.T.);
#6312=ORIENTED_EDGE('',*,*,#4856,.T.);
#6313=ORIENTED_EDGE('',*,*,#4854,.T.);
#6314=ORIENTED_EDGE('',*,*,#4857,.T.);
#6315=ORIENTED_EDGE('',*,*,#4851,.T.);
#6316=ORIENTED_EDGE('',*,*,#4858,.T.);
#6317=ORIENTED_EDGE('',*,*,#4859,.F.);
#6318=ORIENTED_EDGE('',*,*,#4860,.F.);
#6319=ORIENTED_EDGE('',*,*,#4861,.F.);
#6320=ORIENTED_EDGE('',*,*,#4862,.F.);
#6321=ORIENTED_EDGE('',*,*,#4863,.F.);
#6322=ORIENTED_EDGE('',*,*,#4864,.F.);
#6323=ORIENTED_EDGE('',*,*,#4865,.T.);
#6324=ORIENTED_EDGE('',*,*,#4863,.T.);
#6325=ORIENTED_EDGE('',*,*,#4760,.T.);
#6326=ORIENTED_EDGE('',*,*,#4756,.T.);
#6327=ORIENTED_EDGE('',*,*,#4866,.F.);
#6328=ORIENTED_EDGE('',*,*,#4867,.F.);
#6329=ORIENTED_EDGE('',*,*,#4868,.F.);
#6330=ORIENTED_EDGE('',*,*,#4867,.T.);
#6331=ORIENTED_EDGE('',*,*,#4800,.T.);
#6332=ORIENTED_EDGE('',*,*,#4855,.T.);
#6333=ORIENTED_EDGE('',*,*,#4869,.T.);
#6334=ORIENTED_EDGE('',*,*,#4868,.T.);
#6335=ORIENTED_EDGE('',*,*,#4870,.T.);
#6336=ORIENTED_EDGE('',*,*,#4861,.T.);
#6337=ORIENTED_EDGE('',*,*,#4871,.T.);
#6338=ORIENTED_EDGE('',*,*,#4811,.F.);
#6339=ORIENTED_EDGE('',*,*,#4872,.F.);
#6340=ORIENTED_EDGE('',*,*,#4873,.F.);
#6341=ORIENTED_EDGE('',*,*,#4872,.T.);
#6342=ORIENTED_EDGE('',*,*,#4874,.T.);
#6343=ORIENTED_EDGE('',*,*,#4864,.T.);
#6344=ORIENTED_EDGE('',*,*,#4875,.T.);
#6345=ORIENTED_EDGE('',*,*,#4807,.T.);
#6346=ORIENTED_EDGE('',*,*,#4873,.T.);
#6347=ORIENTED_EDGE('',*,*,#4876,.T.);
#6348=ORIENTED_EDGE('',*,*,#4747,.F.);
#6349=ORIENTED_EDGE('',*,*,#4768,.T.);
#6350=ORIENTED_EDGE('',*,*,#4877,.F.);
#6351=ORIENTED_EDGE('',*,*,#4878,.F.);
#6352=ORIENTED_EDGE('',*,*,#4879,.F.);
#6353=ORIENTED_EDGE('',*,*,#4880,.F.);
#6354=ORIENTED_EDGE('',*,*,#4791,.F.);
#6355=ORIENTED_EDGE('',*,*,#4881,.F.);
#6356=ORIENTED_EDGE('',*,*,#4784,.T.);
#6357=ORIENTED_EDGE('',*,*,#4761,.T.);
#6358=ORIENTED_EDGE('',*,*,#4862,.T.);
#6359=ORIENTED_EDGE('',*,*,#4882,.T.);
#6360=ORIENTED_EDGE('',*,*,#4802,.T.);
#6361=ORIENTED_EDGE('',*,*,#4883,.F.);
#6362=ORIENTED_EDGE('',*,*,#4884,.F.);
#6363=ORIENTED_EDGE('',*,*,#4885,.F.);
#6364=ORIENTED_EDGE('',*,*,#4886,.F.);
#6365=ORIENTED_EDGE('',*,*,#4887,.F.);
#6366=ORIENTED_EDGE('',*,*,#4888,.F.);
#6367=ORIENTED_EDGE('',*,*,#4782,.T.);
#6368=ORIENTED_EDGE('',*,*,#4805,.T.);
#6369=ORIENTED_EDGE('',*,*,#4887,.T.);
#6370=ORIENTED_EDGE('',*,*,#4808,.T.);
#6371=ORIENTED_EDGE('',*,*,#4889,.F.);
#6372=ORIENTED_EDGE('',*,*,#4890,.F.);
#6373=ORIENTED_EDGE('',*,*,#4891,.F.);
#6374=ORIENTED_EDGE('',*,*,#4877,.T.);
#6375=ORIENTED_EDGE('',*,*,#4767,.T.);
#6376=ORIENTED_EDGE('',*,*,#4890,.T.);
#6377=ORIENTED_EDGE('',*,*,#4892,.T.);
#6378=ORIENTED_EDGE('',*,*,#4880,.T.);
#6379=ORIENTED_EDGE('',*,*,#4893,.T.);
#6380=ORIENTED_EDGE('',*,*,#4891,.T.);
#6381=ORIENTED_EDGE('',*,*,#4766,.T.);
#6382=ORIENTED_EDGE('',*,*,#4894,.F.);
#6383=ORIENTED_EDGE('',*,*,#4895,.F.);
#6384=ORIENTED_EDGE('',*,*,#4896,.F.);
#6385=ORIENTED_EDGE('',*,*,#4889,.T.);
#6386=ORIENTED_EDGE('',*,*,#4897,.T.);
#6387=ORIENTED_EDGE('',*,*,#4895,.T.);
#6388=ORIENTED_EDGE('',*,*,#4898,.T.);
#6389=ORIENTED_EDGE('',*,*,#4896,.T.);
#6390=ORIENTED_EDGE('',*,*,#4899,.T.);
#6391=ORIENTED_EDGE('',*,*,#4888,.T.);
#6392=ORIENTED_EDGE('',*,*,#4804,.T.);
#6393=ORIENTED_EDGE('',*,*,#4894,.T.);
#6394=ORIENTED_EDGE('',*,*,#4803,.T.);
#6395=ORIENTED_EDGE('',*,*,#4885,.T.);
#6396=ORIENTED_EDGE('',*,*,#4900,.T.);
#6397=ORIENTED_EDGE('',*,*,#4886,.T.);
#6398=ORIENTED_EDGE('',*,*,#4901,.T.);
#6399=ORIENTED_EDGE('',*,*,#4881,.T.);
#6400=ORIENTED_EDGE('',*,*,#4809,.T.);
#6401=ORIENTED_EDGE('',*,*,#4883,.T.);
#6402=ORIENTED_EDGE('',*,*,#4801,.T.);
#6403=ORIENTED_EDGE('',*,*,#4866,.T.);
#6404=ORIENTED_EDGE('',*,*,#4902,.T.);
#6405=ORIENTED_EDGE('',*,*,#4884,.T.);
#6406=ORIENTED_EDGE('',*,*,#4903,.T.);
#6407=ORIENTED_EDGE('',*,*,#4878,.T.);
#6408=ORIENTED_EDGE('',*,*,#4904,.T.);
#6409=ORIENTED_EDGE('',*,*,#4860,.T.);
#6410=ORIENTED_EDGE('',*,*,#4769,.T.);
#6411=ORIENTED_EDGE('',*,*,#4879,.T.);
#6412=ORIENTED_EDGE('',*,*,#4905,.T.);
#6413=ORIENTED_EDGE('',*,*,#4850,.T.);
#6414=ORIENTED_EDGE('',*,*,#4770,.T.);
#6415=ORIENTED_EDGE('',*,*,#4859,.T.);
#6416=ORIENTED_EDGE('',*,*,#4906,.T.);
#6417=ORIENTED_EDGE('',*,*,#4837,.T.);
#6418=ORIENTED_EDGE('',*,*,#4772,.T.);
#6419=ORIENTED_EDGE('',*,*,#4852,.T.);
#6420=ORIENTED_EDGE('',*,*,#4907,.T.);
#6421=ORIENTED_EDGE('',*,*,#4840,.T.);
#6422=ORIENTED_EDGE('',*,*,#4908,.T.);
#6423=ORIENTED_EDGE('',*,*,#4849,.T.);
#6424=ORIENTED_EDGE('',*,*,#4755,.T.);
#6425=ORIENTED_EDGE('',*,*,#4848,.T.);
#6426=ORIENTED_EDGE('',*,*,#4909,.T.);
#6427=ORIENTED_EDGE('',*,*,#4831,.T.);
#6428=ORIENTED_EDGE('',*,*,#4792,.T.);
#6429=ORIENTED_EDGE('',*,*,#4821,.T.);
#6430=ORIENTED_EDGE('',*,*,#4910,.T.);
#6431=ORIENTED_EDGE('',*,*,#4841,.T.);
#6432=ORIENTED_EDGE('',*,*,#4778,.T.);
#6433=ORIENTED_EDGE('',*,*,#4819,.T.);
#6434=ORIENTED_EDGE('',*,*,#4774,.T.);
#6435=ORIENTED_EDGE('',*,*,#4839,.T.);
#6436=ORIENTED_EDGE('',*,*,#4911,.T.);
#6437=ORIENTED_EDGE('',*,*,#4812,.T.);
#6438=ORIENTED_EDGE('',*,*,#4775,.T.);
#6439=ORIENTED_EDGE('',*,*,#4818,.T.);
#6440=ORIENTED_EDGE('',*,*,#4912,.T.);
#6441=ORIENTED_EDGE('',*,*,#4816,.T.);
#6442=ORIENTED_EDGE('',*,*,#4913,.T.);
#6443=ORIENTED_EDGE('',*,*,#4813,.T.);
#6444=ORIENTED_EDGE('',*,*,#4914,.T.);
#6445=ORIENTED_EDGE('',*,*,#4876,.F.);
#6446=ORIENTED_EDGE('',*,*,#4875,.F.);
#6447=ORIENTED_EDGE('',*,*,#4865,.F.);
#6448=ORIENTED_EDGE('',*,*,#4752,.F.);
#6449=ORIENTED_EDGE('',*,*,#4824,.F.);
#6450=ORIENTED_EDGE('',*,*,#4913,.F.);
#6451=ORIENTED_EDGE('',*,*,#4836,.F.);
#6452=ORIENTED_EDGE('',*,*,#4835,.F.);
#6453=ORIENTED_EDGE('',*,*,#4828,.F.);
#6454=ORIENTED_EDGE('',*,*,#4914,.F.);
#6455=ORIENTED_EDGE('',*,*,#4912,.F.);
#6456=ORIENTED_EDGE('',*,*,#4829,.F.);
#6457=ORIENTED_EDGE('',*,*,#4830,.F.);
#6458=ORIENTED_EDGE('',*,*,#4911,.F.);
#6459=ORIENTED_EDGE('',*,*,#4846,.F.);
#6460=ORIENTED_EDGE('',*,*,#4845,.F.);
#6461=ORIENTED_EDGE('',*,*,#4847,.F.);
#6462=ORIENTED_EDGE('',*,*,#4907,.F.);
#6463=ORIENTED_EDGE('',*,*,#4857,.F.);
#6464=ORIENTED_EDGE('',*,*,#4856,.F.);
#6465=ORIENTED_EDGE('',*,*,#4858,.F.);
#6466=ORIENTED_EDGE('',*,*,#4906,.F.);
#6467=ORIENTED_EDGE('',*,*,#4870,.F.);
#6468=ORIENTED_EDGE('',*,*,#4869,.F.);
#6469=ORIENTED_EDGE('',*,*,#4871,.F.);
#6470=ORIENTED_EDGE('',*,*,#4905,.F.);
#6471=ORIENTED_EDGE('',*,*,#4903,.F.);
#6472=ORIENTED_EDGE('',*,*,#4902,.F.);
#6473=ORIENTED_EDGE('',*,*,#4785,.T.);
#6474=ORIENTED_EDGE('',*,*,#4882,.F.);
#6475=ORIENTED_EDGE('',*,*,#4874,.F.);
#6476=ORIENTED_EDGE('',*,*,#4810,.F.);
#6477=ORIENTED_EDGE('',*,*,#4892,.F.);
#6478=ORIENTED_EDGE('',*,*,#4898,.F.);
#6479=ORIENTED_EDGE('',*,*,#4900,.F.);
#6480=ORIENTED_EDGE('',*,*,#4904,.F.);
#6481=ORIENTED_EDGE('',*,*,#4893,.F.);
#6482=ORIENTED_EDGE('',*,*,#4901,.F.);
#6483=ORIENTED_EDGE('',*,*,#4899,.F.);
#6484=ORIENTED_EDGE('',*,*,#4897,.F.);
#6485=ORIENTED_EDGE('',*,*,#4908,.F.);
#6486=ORIENTED_EDGE('',*,*,#4910,.F.);
#6487=ORIENTED_EDGE('',*,*,#4834,.F.);
#6488=ORIENTED_EDGE('',*,*,#4909,.F.);
#8868=PLANE('',#9765);
#8869=PLANE('',#9768);
#8870=PLANE('',#9771);
#8871=PLANE('',#9776);
#8872=PLANE('',#9777);
#8873=PLANE('',#9782);
#8874=PLANE('',#9787);
#8875=PLANE('',#9790);
#8876=PLANE('',#9793);
#8877=PLANE('',#9796);
#8878=PLANE('',#9801);
#8879=PLANE('',#9921);
#8880=PLANE('',#9922);
#8881=PLANE('',#9923);
#8882=PLANE('',#9924);
#8883=PLANE('',#9925);
#8884=PLANE('',#9926);
#8885=PLANE('',#9927);
#8886=PLANE('',#9928);
#8887=PLANE('',#9929);
#8888=PLANE('',#9930);
#8889=PLANE('',#9931);
#9021=ADVANCED_FACE('',(#2034),#8868,.T.);
#9022=ADVANCED_FACE('',(#2035),#8869,.T.);
#9023=ADVANCED_FACE('',(#2036),#8870,.T.);
#9024=ADVANCED_FACE('',(#2037),#329,.T.);
#9025=ADVANCED_FACE('',(#2038),#330,.T.);
#9026=ADVANCED_FACE('',(#2039),#8871,.T.);
#9027=ADVANCED_FACE('',(#2040),#8872,.T.);
#9028=ADVANCED_FACE('',(#2041),#331,.T.);
#9029=ADVANCED_FACE('',(#2042),#332,.T.);
#9030=ADVANCED_FACE('',(#2043),#8873,.T.);
#9031=ADVANCED_FACE('',(#2044),#8874,.F.);
#9032=ADVANCED_FACE('',(#2045),#8875,.F.);
#9033=ADVANCED_FACE('',(#2046),#8876,.F.);
#9034=ADVANCED_FACE('',(#2047),#333,.T.);
#9035=ADVANCED_FACE('',(#2048),#8877,.T.);
#9036=ADVANCED_FACE('',(#2049),#8878,.T.);
#9037=ADVANCED_FACE('',(#2050),#334,.T.);
#9038=ADVANCED_FACE('',(#2051),#211,.T.);
#9039=ADVANCED_FACE('',(#2052),#212,.T.);
#9040=ADVANCED_FACE('',(#2053),#119,.T.);
#9041=ADVANCED_FACE('',(#2054),#120,.T.);
#9042=ADVANCED_FACE('',(#2055),#335,.T.);
#9043=ADVANCED_FACE('',(#2056),#121,.T.);
#9044=ADVANCED_FACE('',(#2057),#336,.T.);
#9045=ADVANCED_FACE('',(#2058),#337,.T.);
#9046=ADVANCED_FACE('',(#2059),#122,.T.);
#9047=ADVANCED_FACE('',(#2060),#338,.T.);
#9048=ADVANCED_FACE('',(#2061),#339,.T.);
#9049=ADVANCED_FACE('',(#2062),#213,.T.);
#9050=ADVANCED_FACE('',(#2063),#123,.T.);
#9051=ADVANCED_FACE('',(#2064),#214,.T.);
#9052=ADVANCED_FACE('',(#2065),#340,.T.);
#9053=ADVANCED_FACE('',(#2066),#341,.F.);
#9054=ADVANCED_FACE('',(#2067),#124,.T.);
#9055=ADVANCED_FACE('',(#2068),#215,.T.);
#9056=ADVANCED_FACE('',(#2069),#216,.T.);
#9057=ADVANCED_FACE('',(#2070),#342,.T.);
#9058=ADVANCED_FACE('',(#2071),#343,.F.);
#9059=ADVANCED_FACE('',(#2072),#125,.T.);
#9060=ADVANCED_FACE('',(#2073),#126,.T.);
#9061=ADVANCED_FACE('',(#2074),#344,.T.);
#9062=ADVANCED_FACE('',(#2075),#127,.T.);
#9063=ADVANCED_FACE('',(#2076),#345,.T.);
#9064=ADVANCED_FACE('',(#2077),#346,.T.);
#9065=ADVANCED_FACE('',(#2078),#128,.T.);
#9066=ADVANCED_FACE('',(#2079),#347,.T.);
#9067=ADVANCED_FACE('',(#2080),#348,.T.);
#9068=ADVANCED_FACE('',(#2081),#217,.T.);
#9069=ADVANCED_FACE('',(#2082),#129,.T.);
#9070=ADVANCED_FACE('',(#2083),#349,.T.);
#9071=ADVANCED_FACE('',(#2084),#218,.T.);
#9072=ADVANCED_FACE('',(#2085),#130,.T.);
#9073=ADVANCED_FACE('',(#2086),#350,.T.);
#9074=ADVANCED_FACE('',(#2087),#131,.T.);
#9075=ADVANCED_FACE('',(#2088),#351,.T.);
#9076=ADVANCED_FACE('',(#2089),#352,.T.);
#9077=ADVANCED_FACE('',(#2090),#132,.T.);
#9078=ADVANCED_FACE('',(#2091),#353,.T.);
#9079=ADVANCED_FACE('',(#2092),#354,.T.);
#9080=ADVANCED_FACE('',(#2093),#355,.T.);
#9081=ADVANCED_FACE('',(#2094),#356,.T.);
#9082=ADVANCED_FACE('',(#2095),#357,.T.);
#9083=ADVANCED_FACE('',(#2096),#358,.F.);
#9084=ADVANCED_FACE('',(#2097),#359,.T.);
#9085=ADVANCED_FACE('',(#2098),#360,.T.);
#9086=ADVANCED_FACE('',(#2099),#361,.T.);
#9087=ADVANCED_FACE('',(#2100),#362,.T.);
#9088=ADVANCED_FACE('',(#2101),#363,.T.);
#9089=ADVANCED_FACE('',(#2102),#364,.T.);
#9090=ADVANCED_FACE('',(#2103),#365,.T.);
#9091=ADVANCED_FACE('',(#2104),#366,.T.);
#9092=ADVANCED_FACE('',(#2105),#367,.F.);
#9093=ADVANCED_FACE('',(#2106),#8879,.F.);
#9094=ADVANCED_FACE('',(#2107),#8880,.F.);
#9095=ADVANCED_FACE('',(#2108),#8881,.F.);
#9096=ADVANCED_FACE('',(#2109),#8882,.F.);
#9097=ADVANCED_FACE('',(#2110),#8883,.F.);
#9098=ADVANCED_FACE('',(#2111),#8884,.F.);
#9099=ADVANCED_FACE('',(#2112),#8885,.F.);
#9100=ADVANCED_FACE('',(#2113),#8886,.T.);
#9101=ADVANCED_FACE('',(#2114),#8887,.F.);
#9102=ADVANCED_FACE('',(#2115),#8888,.T.);
#9103=ADVANCED_FACE('',(#2116),#8889,.T.);
#9629=CLOSED_SHELL('',(#9021,#9022,#9023,#9024,#9025,#9026,#9027,#9028,
#9029,#9030,#9031,#9032,#9033,#9034,#9035,#9036,#9037,#9038,#9039,#9040,
#9041,#9042,#9043,#9044,#9045,#9046,#9047,#9048,#9049,#9050,#9051,#9052,
#9053,#9054,#9055,#9056,#9057,#9058,#9059,#9060,#9061,#9062,#9063,#9064,
#9065,#9066,#9067,#9068,#9069,#9070,#9071,#9072,#9073,#9074,#9075,#9076,
#9077,#9078,#9079,#9080,#9081,#9082,#9083,#9084,#9085,#9086,#9087,#9088,
#9089,#9090,#9091,#9092,#9093,#9094,#9095,#9096,#9097,#9098,#9099,#9100,
#9101,#9102,#9103));
#9764=AXIS2_PLACEMENT_3D('',#14288,#11066,#11067);
#9765=AXIS2_PLACEMENT_3D('',#14289,#11068,#11069);
#9766=AXIS2_PLACEMENT_3D('',#14292,#11070,#11071);
#9767=AXIS2_PLACEMENT_3D('',#14300,#11075,#11076);
#9768=AXIS2_PLACEMENT_3D('',#14302,#11078,#11079);
#9769=AXIS2_PLACEMENT_3D('',#14305,#11080,#11081);
#9770=AXIS2_PLACEMENT_3D('',#14309,#11083,#11084);
#9771=AXIS2_PLACEMENT_3D('',#14315,#11088,#11089);
#9772=AXIS2_PLACEMENT_3D('',#14318,#11092,#11093);
#9773=AXIS2_PLACEMENT_3D('',#14322,#11095,#11096);
#9774=AXIS2_PLACEMENT_3D('',#14324,#11098,#11099);
#9775=AXIS2_PLACEMENT_3D('',#14328,#11101,#11102);
#9776=AXIS2_PLACEMENT_3D('',#14330,#11104,#11105);
#9777=AXIS2_PLACEMENT_3D('',#14334,#11108,#11109);
#9778=AXIS2_PLACEMENT_3D('',#14338,#11112,#11113);
#9779=AXIS2_PLACEMENT_3D('',#14340,#11114,#11115);
#9780=AXIS2_PLACEMENT_3D('',#14342,#11117,#11118);
#9781=AXIS2_PLACEMENT_3D('',#14345,#11120,#11121);
#9782=AXIS2_PLACEMENT_3D('',#14346,#11122,#11123);
#9783=AXIS2_PLACEMENT_3D('',#14364,#11132,#11133);
#9784=AXIS2_PLACEMENT_3D('',#14370,#11136,#11137);
#9785=AXIS2_PLACEMENT_3D('',#14374,#11139,#11140);
#9786=AXIS2_PLACEMENT_3D('',#14380,#11143,#11144);
#9787=AXIS2_PLACEMENT_3D('',#14384,#11147,#11148);
#9788=AXIS2_PLACEMENT_3D('',#14386,#11149,#11150);
#9789=AXIS2_PLACEMENT_3D('',#14392,#11153,#11154);
#9790=AXIS2_PLACEMENT_3D('',#14394,#11156,#11157);
#9791=AXIS2_PLACEMENT_3D('',#14396,#11158,#11159);
#9792=AXIS2_PLACEMENT_3D('',#14400,#11161,#11162);
#9793=AXIS2_PLACEMENT_3D('',#14404,#11165,#11166);
#9794=AXIS2_PLACEMENT_3D('',#14406,#11168,#11169);
#9795=AXIS2_PLACEMENT_3D('',#14409,#11171,#11172);
#9796=AXIS2_PLACEMENT_3D('',#14410,#11173,#11174);
#9797=AXIS2_PLACEMENT_3D('',#14416,#11177,#11178);
#9798=AXIS2_PLACEMENT_3D('',#14422,#11181,#11182);
#9799=AXIS2_PLACEMENT_3D('',#14426,#11184,#11185);
#9800=AXIS2_PLACEMENT_3D('',#14432,#11188,#11189);
#9801=AXIS2_PLACEMENT_3D('',#14441,#11195,#11196);
#9802=AXIS2_PLACEMENT_3D('',#14445,#11199,#11200);
#9803=AXIS2_PLACEMENT_3D('',#14448,#11202,#11203);
#9804=AXIS2_PLACEMENT_3D('',#14449,#11204,#11205);
#9805=AXIS2_PLACEMENT_3D('',#14451,#11206,#11207);
#9806=AXIS2_PLACEMENT_3D('',#14453,#11208,#11209);
#9807=AXIS2_PLACEMENT_3D('',#14454,#11210,#11211);
#9808=AXIS2_PLACEMENT_3D('',#14455,#11212,#11213);
#9809=AXIS2_PLACEMENT_3D('',#14457,#11214,#11215);
#9810=AXIS2_PLACEMENT_3D('',#14459,#11216,#11217);
#9811=AXIS2_PLACEMENT_3D('',#14460,#11218,#11219);
#9812=AXIS2_PLACEMENT_3D('',#14461,#11220,#11221);
#9813=AXIS2_PLACEMENT_3D('',#14463,#11222,#11223);
#9814=AXIS2_PLACEMENT_3D('',#14465,#11224,#11225);
#9815=AXIS2_PLACEMENT_3D('',#14466,#11226,#11227);
#9816=AXIS2_PLACEMENT_3D('',#14467,#11228,#11229);
#9817=AXIS2_PLACEMENT_3D('',#14469,#11230,#11231);
#9818=AXIS2_PLACEMENT_3D('',#14471,#11232,#11233);
#9819=AXIS2_PLACEMENT_3D('',#14472,#11234,#11235);
#9820=AXIS2_PLACEMENT_3D('',#14473,#11236,#11237);
#9821=AXIS2_PLACEMENT_3D('',#14475,#11239,#11240);
#9822=AXIS2_PLACEMENT_3D('',#14477,#11241,#11242);
#9823=AXIS2_PLACEMENT_3D('',#14479,#11243,#11244);
#9824=AXIS2_PLACEMENT_3D('',#14480,#11245,#11246);
#9825=AXIS2_PLACEMENT_3D('',#14481,#11247,#11248);
#9826=AXIS2_PLACEMENT_3D('',#14483,#11250,#11251);
#9827=AXIS2_PLACEMENT_3D('',#14486,#11254,#11255);
#9828=AXIS2_PLACEMENT_3D('',#14488,#11256,#11257);
#9829=AXIS2_PLACEMENT_3D('',#14490,#11258,#11259);
#9830=AXIS2_PLACEMENT_3D('',#14491,#11260,#11261);
#9831=AXIS2_PLACEMENT_3D('',#14492,#11262,#11263);
#9832=AXIS2_PLACEMENT_3D('',#14495,#11266,#11267);
#9833=AXIS2_PLACEMENT_3D('',#14497,#11269,#11270);
#9834=AXIS2_PLACEMENT_3D('',#14499,#11271,#11272);
#9835=AXIS2_PLACEMENT_3D('',#14501,#11273,#11274);
#9836=AXIS2_PLACEMENT_3D('',#14502,#11275,#11276);
#9837=AXIS2_PLACEMENT_3D('',#14503,#11277,#11278);
#9838=AXIS2_PLACEMENT_3D('',#14505,#11279,#11280);
#9839=AXIS2_PLACEMENT_3D('',#14506,#11281,#11282);
#9840=AXIS2_PLACEMENT_3D('',#14507,#11283,#11284);
#9841=AXIS2_PLACEMENT_3D('',#14509,#11285,#11286);
#9842=AXIS2_PLACEMENT_3D('',#14511,#11287,#11288);
#9843=AXIS2_PLACEMENT_3D('',#14512,#11289,#11290);
#9844=AXIS2_PLACEMENT_3D('',#14513,#11291,#11292);
#9845=AXIS2_PLACEMENT_3D('',#14515,#11294,#11295);
#9846=AXIS2_PLACEMENT_3D('',#14518,#11298,#11299);
#9847=AXIS2_PLACEMENT_3D('',#14520,#11300,#11301);
#9848=AXIS2_PLACEMENT_3D('',#14521,#11302,#11303);
#9849=AXIS2_PLACEMENT_3D('',#14522,#11304,#11305);
#9850=AXIS2_PLACEMENT_3D('',#14524,#11306,#11307);
#9851=AXIS2_PLACEMENT_3D('',#14526,#11308,#11309);
#9852=AXIS2_PLACEMENT_3D('',#14527,#11310,#11311);
#9853=AXIS2_PLACEMENT_3D('',#14528,#11312,#11313);
#9854=AXIS2_PLACEMENT_3D('',#14530,#11314,#11315);
#9855=AXIS2_PLACEMENT_3D('',#14532,#11316,#11317);
#9856=AXIS2_PLACEMENT_3D('',#14533,#11318,#11319);
#9857=AXIS2_PLACEMENT_3D('',#14534,#11320,#11321);
#9858=AXIS2_PLACEMENT_3D('',#14536,#11323,#11324);
#9859=AXIS2_PLACEMENT_3D('',#14539,#11327,#11328);
#9860=AXIS2_PLACEMENT_3D('',#14541,#11329,#11330);
#9861=AXIS2_PLACEMENT_3D('',#14543,#11331,#11332);
#9862=AXIS2_PLACEMENT_3D('',#14544,#11333,#11334);
#9863=AXIS2_PLACEMENT_3D('',#14545,#11335,#11336);
#9864=AXIS2_PLACEMENT_3D('',#14547,#11337,#11338);
#9865=AXIS2_PLACEMENT_3D('',#14549,#11339,#11340);
#9866=AXIS2_PLACEMENT_3D('',#14550,#11341,#11342);
#9867=AXIS2_PLACEMENT_3D('',#14551,#11343,#11344);
#9868=AXIS2_PLACEMENT_3D('',#14553,#11346,#11347);
#9869=AXIS2_PLACEMENT_3D('',#14555,#11348,#11349);
#9870=AXIS2_PLACEMENT_3D('',#14557,#11350,#11351);
#9871=AXIS2_PLACEMENT_3D('',#14558,#11352,#11353);
#9872=AXIS2_PLACEMENT_3D('',#14559,#11354,#11355);
#9873=AXIS2_PLACEMENT_3D('',#14561,#11357,#11358);
#9874=AXIS2_PLACEMENT_3D('',#14564,#11361,#11362);
#9875=AXIS2_PLACEMENT_3D('',#14566,#11363,#11364);
#9876=AXIS2_PLACEMENT_3D('',#14567,#11365,#11366);
#9877=AXIS2_PLACEMENT_3D('',#14568,#11367,#11368);
#9878=AXIS2_PLACEMENT_3D('',#14571,#11371,#11372);
#9879=AXIS2_PLACEMENT_3D('',#14573,#11374,#11375);
#9880=AXIS2_PLACEMENT_3D('',#14575,#11376,#11377);
#9881=AXIS2_PLACEMENT_3D('',#14577,#11378,#11379);
#9882=AXIS2_PLACEMENT_3D('',#14578,#11380,#11381);
#9883=AXIS2_PLACEMENT_3D('',#14579,#11382,#11383);
#9884=AXIS2_PLACEMENT_3D('',#14581,#11384,#11385);
#9885=AXIS2_PLACEMENT_3D('',#14582,#11386,#11387);
#9886=AXIS2_PLACEMENT_3D('',#14583,#11388,#11389);
#9887=AXIS2_PLACEMENT_3D('',#14585,#11391,#11392);
#9888=AXIS2_PLACEMENT_3D('',#14587,#11393,#11394);
#9889=AXIS2_PLACEMENT_3D('',#14589,#11395,#11396);
#9890=AXIS2_PLACEMENT_3D('',#14590,#11397,#11398);
#9891=AXIS2_PLACEMENT_3D('',#14591,#11399,#11400);
#9892=AXIS2_PLACEMENT_3D('',#14593,#11401,#11402);
#9893=AXIS2_PLACEMENT_3D('',#14594,#11403,#11404);
#9894=AXIS2_PLACEMENT_3D('',#14595,#11405,#11406);
#9895=AXIS2_PLACEMENT_3D('',#14596,#11407,#11408);
#9896=AXIS2_PLACEMENT_3D('',#14597,#11409,#11410);
#9897=AXIS2_PLACEMENT_3D('',#14600,#11411,#11412);
#9898=AXIS2_PLACEMENT_3D('',#14601,#11413,#11414);
#9899=AXIS2_PLACEMENT_3D('',#14602,#11415,#11416);
#9900=AXIS2_PLACEMENT_3D('',#14603,#11417,#11418);
#9901=AXIS2_PLACEMENT_3D('',#14605,#11420,#11421);
#9902=AXIS2_PLACEMENT_3D('',#14607,#11423,#11424);
#9903=AXIS2_PLACEMENT_3D('',#14609,#11425,#11426);
#9904=AXIS2_PLACEMENT_3D('',#14611,#11427,#11428);
#9905=AXIS2_PLACEMENT_3D('',#14612,#11429,#11430);
#9906=AXIS2_PLACEMENT_3D('',#14613,#11431,#11432);
#9907=AXIS2_PLACEMENT_3D('',#14616,#11435,#11436);
#9908=AXIS2_PLACEMENT_3D('',#14618,#11438,#11439);
#9909=AXIS2_PLACEMENT_3D('',#14620,#11441,#11442);
#9910=AXIS2_PLACEMENT_3D('',#14622,#11444,#11445);
#9911=AXIS2_PLACEMENT_3D('',#14624,#11447,#11448);
#9912=AXIS2_PLACEMENT_3D('',#14627,#11451,#11452);
#9913=AXIS2_PLACEMENT_3D('',#14629,#11454,#11455);
#9914=AXIS2_PLACEMENT_3D('',#14631,#11457,#11458);
#9915=AXIS2_PLACEMENT_3D('',#14633,#11460,#11461);
#9916=AXIS2_PLACEMENT_3D('',#14635,#11463,#11464);
#9917=AXIS2_PLACEMENT_3D('',#14637,#11466,#11467);
#9918=AXIS2_PLACEMENT_3D('',#14639,#11469,#11470);
#9919=AXIS2_PLACEMENT_3D('',#14641,#11472,#11473);
#9920=AXIS2_PLACEMENT_3D('',#14643,#11475,#11476);
#9921=AXIS2_PLACEMENT_3D('',#14646,#11479,#11480);
#9922=AXIS2_PLACEMENT_3D('',#14647,#11481,#11482);
#9923=AXIS2_PLACEMENT_3D('',#14648,#11483,#11484);
#9924=AXIS2_PLACEMENT_3D('',#14649,#11485,#11486);
#9925=AXIS2_PLACEMENT_3D('',#14650,#11487,#11488);
#9926=AXIS2_PLACEMENT_3D('',#14651,#11489,#11490);
#9927=AXIS2_PLACEMENT_3D('',#14652,#11491,#11492);
#9928=AXIS2_PLACEMENT_3D('',#14653,#11493,#11494);
#9929=AXIS2_PLACEMENT_3D('',#14654,#11495,#11496);
#9930=AXIS2_PLACEMENT_3D('',#14655,#11497,#11498);
#9931=AXIS2_PLACEMENT_3D('',#14656,#11499,#11500);
#11066=DIRECTION('axis',(0.,0.,1.));
#11067=DIRECTION('refdir',(1.,0.,0.));
#11068=DIRECTION('center_axis',(0.,0.,-1.));
#11069=DIRECTION('ref_axis',(-1.,0.,0.));
#11070=DIRECTION('center_axis',(0.,0.,1.));
#11071=DIRECTION('ref_axis',(0.707106781186548,-0.707106781186548,0.));
#11072=DIRECTION('',(1.,0.,0.));
#11073=DIRECTION('',(0.,1.,0.));
#11074=DIRECTION('',(-1.,0.,0.));
#11075=DIRECTION('center_axis',(0.,0.,1.));
#11076=DIRECTION('ref_axis',(0.707106781186548,0.707106781186548,0.));
#11077=DIRECTION('',(0.,1.,0.));
#11078=DIRECTION('center_axis',(0.,0.,1.));
#11079=DIRECTION('ref_axis',(1.,0.,0.));
#11080=DIRECTION('center_axis',(0.,0.,-1.));
#11081=DIRECTION('ref_axis',(0.707106781186548,-0.707106781186548,0.));
#11082=DIRECTION('',(0.,-1.,0.));
#11083=DIRECTION('center_axis',(0.,0.,-1.));
#11084=DIRECTION('ref_axis',(0.707106781186548,0.707106781186548,0.));
#11085=DIRECTION('',(1.,0.,0.));
#11086=DIRECTION('',(0.,1.,0.));
#11087=DIRECTION('',(-1.,0.,0.));
#11088=DIRECTION('center_axis',(1.,0.,0.));
#11089=DIRECTION('ref_axis',(0.,0.,-1.));
#11090=DIRECTION('',(0.,0.,-1.));
#11091=DIRECTION('',(0.,0.,1.));
#11092=DIRECTION('center_axis',(0.,0.,1.));
#11093=DIRECTION('ref_axis',(0.707106781186548,-0.707106781186548,0.));
#11094=DIRECTION('',(0.,0.,-1.));
#11095=DIRECTION('center_axis',(0.707106781186543,0.,0.707106781186553));
#11096=DIRECTION('ref_axis',(0.707106781186553,0.,-0.707106781186543));
#11097=DIRECTION('',(0.,0.,1.));
#11098=DIRECTION('center_axis',(0.,0.,1.));
#11099=DIRECTION('ref_axis',(0.707106781186548,-0.707106781186548,0.));
#11100=DIRECTION('',(0.,0.,1.));
#11101=DIRECTION('center_axis',(0.,0.,1.));
#11102=DIRECTION('ref_axis',(1.,0.,0.));
#11103=DIRECTION('',(0.,0.,-1.));
#11104=DIRECTION('center_axis',(1.,0.,0.));
#11105=DIRECTION('ref_axis',(0.,1.,0.));
#11106=DIRECTION('',(0.,1.,0.));
#11107=DIRECTION('',(0.,0.,-1.));
#11108=DIRECTION('center_axis',(1.,0.,0.));
#11109=DIRECTION('ref_axis',(0.,1.,0.));
#11110=DIRECTION('',(0.,0.,-1.));
#11111=DIRECTION('',(0.,1.,0.));
#11112=DIRECTION('center_axis',(0.,0.,1.));
#11113=DIRECTION('ref_axis',(0.707106781186548,0.707106781186548,0.));
#11114=DIRECTION('center_axis',(-0.707106781186543,0.,-0.707106781186553));
#11115=DIRECTION('ref_axis',(0.707106781186553,0.,-0.707106781186542));
#11116=DIRECTION('',(0.,0.,1.));
#11117=DIRECTION('center_axis',(0.,0.,1.));
#11118=DIRECTION('ref_axis',(0.707106781186548,0.707106781186548,0.));
#11119=DIRECTION('',(0.,0.,1.));
#11120=DIRECTION('center_axis',(0.,0.,1.));
#11121=DIRECTION('ref_axis',(0.,1.,0.));
#11122=DIRECTION('center_axis',(0.,1.,0.));
#11123=DIRECTION('ref_axis',(-1.,0.,0.));
#11124=DIRECTION('',(1.,0.,0.));
#11125=DIRECTION('',(0.,0.,-1.));
#11126=DIRECTION('',(1.,0.,0.));
#11127=DIRECTION('',(0.,0.,1.));
#11128=DIRECTION('',(-1.,0.,0.));
#11129=DIRECTION('',(0.,0.,-1.));
#11130=DIRECTION('',(-1.,0.,0.));
#11131=DIRECTION('',(0.707106781186548,0.,0.707106781186548));
#11132=DIRECTION('center_axis',(0.,1.,0.));
#11133=DIRECTION('ref_axis',(-0.923879532511307,0.,-0.38268343236504));
#11134=DIRECTION('',(-1.,0.,0.));
#11135=DIRECTION('',(0.,0.,1.));
#11136=DIRECTION('center_axis',(0.,1.,0.));
#11137=DIRECTION('ref_axis',(-0.70710678118655,0.,-0.707106781186544));
#11138=DIRECTION('',(-1.,0.,0.));
#11139=DIRECTION('center_axis',(0.,1.,0.));
#11140=DIRECTION('ref_axis',(0.707106781186546,0.,-0.707106781186549));
#11141=DIRECTION('',(0.,0.,-1.));
#11142=DIRECTION('',(-1.,0.,0.));
#11143=DIRECTION('center_axis',(0.,1.,0.));
#11144=DIRECTION('ref_axis',(0.707106781186546,0.,-0.707106781186549));
#11145=DIRECTION('',(0.,0.,-1.));
#11146=DIRECTION('',(-1.,0.,0.));
#11147=DIRECTION('center_axis',(0.,0.,1.));
#11148=DIRECTION('ref_axis',(1.,0.,0.));
#11149=DIRECTION('center_axis',(0.,0.,1.));
#11150=DIRECTION('ref_axis',(-0.707106781186548,0.707106781186548,0.));
#11151=DIRECTION('',(0.,1.,0.));
#11152=DIRECTION('',(1.,0.,0.));
#11153=DIRECTION('center_axis',(0.,0.,1.));
#11154=DIRECTION('ref_axis',(-0.707106781186548,-0.707106781186548,0.));
#11155=DIRECTION('',(0.,-1.,0.));
#11156=DIRECTION('center_axis',(0.,0.,-1.));
#11157=DIRECTION('ref_axis',(-1.,0.,0.));
#11158=DIRECTION('center_axis',(0.,0.,-1.));
#11159=DIRECTION('ref_axis',(-0.707106781186548,0.707106781186548,0.));
#11160=DIRECTION('',(0.,1.,0.));
#11161=DIRECTION('center_axis',(0.,0.,-1.));
#11162=DIRECTION('ref_axis',(-0.707106781186548,-0.707106781186548,0.));
#11163=DIRECTION('',(-1.,0.,0.));
#11164=DIRECTION('',(0.,1.,0.));
#11165=DIRECTION('center_axis',(1.,0.,0.));
#11166=DIRECTION('ref_axis',(0.,0.,-1.));
#11167=DIRECTION('',(0.,0.,-1.));
#11168=DIRECTION('center_axis',(0.,0.,1.));
#11169=DIRECTION('ref_axis',(-0.707106781186548,0.707106781186548,0.));
#11170=DIRECTION('',(0.,0.,1.));
#11171=DIRECTION('center_axis',(0.,0.,1.));
#11172=DIRECTION('ref_axis',(-1.,0.,0.));
#11173=DIRECTION('center_axis',(0.,-1.,0.));
#11174=DIRECTION('ref_axis',(1.,0.,0.));
#11175=DIRECTION('',(1.,0.,0.));
#11176=DIRECTION('',(0.,0.,1.));
#11177=DIRECTION('center_axis',(0.,-1.,0.));
#11178=DIRECTION('ref_axis',(0.707106781186552,0.,-0.707106781186543));
#11179=DIRECTION('',(1.,0.,0.));
#11180=DIRECTION('',(0.,0.,1.));
#11181=DIRECTION('center_axis',(0.,-1.,0.));
#11182=DIRECTION('ref_axis',(0.707106781186546,0.,-0.707106781186549));
#11183=DIRECTION('',(1.,0.,0.));
#11184=DIRECTION('center_axis',(0.,-1.,0.));
#11185=DIRECTION('ref_axis',(-0.707106781186547,0.,-0.707106781186547));
#11186=DIRECTION('',(0.,0.,-1.));
#11187=DIRECTION('',(1.,0.,0.));
#11188=DIRECTION('center_axis',(0.,-1.,0.));
#11189=DIRECTION('ref_axis',(-0.923879532511279,0.,-0.382683432365108));
#11190=DIRECTION('',(-0.707106781186548,0.,-0.707106781186548));
#11191=DIRECTION('',(1.,0.,0.));
#11192=DIRECTION('',(0.,0.,1.));
#11193=DIRECTION('',(0.,0.,1.));
#11194=DIRECTION('',(-1.,0.,0.));
#11195=DIRECTION('center_axis',(-1.,0.,0.));
#11196=DIRECTION('ref_axis',(0.,-1.,0.));
#11197=DIRECTION('',(0.,0.,-1.));
#11198=DIRECTION('',(0.,-1.,0.));
#11199=DIRECTION('center_axis',(0.,0.,1.));
#11200=DIRECTION('ref_axis',(-0.707106781186548,-0.707106781186548,0.));
#11201=DIRECTION('',(0.,0.,-1.));
#11202=DIRECTION('center_axis',(0.,0.,-1.));
#11203=DIRECTION('ref_axis',(-1.,0.,0.));
#11204=DIRECTION('center_axis',(0.,1.,0.));
#11205=DIRECTION('ref_axis',(0.,0.,1.));
#11206=DIRECTION('center_axis',(-1.,0.,0.));
#11207=DIRECTION('ref_axis',(0.,0.,1.));
#11208=DIRECTION('center_axis',(0.,-1.,0.));
#11209=DIRECTION('ref_axis',(1.,0.,0.));
#11210=DIRECTION('center_axis',(0.,0.,1.));
#11211=DIRECTION('ref_axis',(0.,1.,0.));
#11212=DIRECTION('center_axis',(0.,-1.,0.));
#11213=DIRECTION('ref_axis',(0.,0.,-1.));
#11214=DIRECTION('center_axis',(0.,0.,1.));
#11215=DIRECTION('ref_axis',(-1.,0.,0.));
#11216=DIRECTION('center_axis',(0.,1.,0.));
#11217=DIRECTION('ref_axis',(0.,0.,-1.));
#11218=DIRECTION('center_axis',(-1.,0.,0.));
#11219=DIRECTION('ref_axis',(0.,-1.,0.));
#11220=DIRECTION('center_axis',(-0.81649658092773,-0.408248290463861,-0.408248290463858));
#11221=DIRECTION('ref_axis',(-0.577350269189626,0.577350269189626,0.577350269189626));
#11222=DIRECTION('center_axis',(-1.,0.,0.));
#11223=DIRECTION('ref_axis',(0.,1.,0.));
#11224=DIRECTION('center_axis',(0.,0.,1.));
#11225=DIRECTION('ref_axis',(-1.,0.,0.));
#11226=DIRECTION('center_axis',(0.,1.,0.));
#11227=DIRECTION('ref_axis',(0.,0.,1.));
#11228=DIRECTION('center_axis',(-0.816496580927728,-0.408248290463864,-0.408248290463857));
#11229=DIRECTION('ref_axis',(-0.577350269189628,0.577350269189628,0.577350269189621));
#11230=DIRECTION('center_axis',(-1.,0.,0.));
#11231=DIRECTION('ref_axis',(0.,1.,0.));
#11232=DIRECTION('center_axis',(0.,4.44089209850056E-15,1.));
#11233=DIRECTION('ref_axis',(-1.,0.,0.));
#11234=DIRECTION('center_axis',(0.,1.,0.));
#11235=DIRECTION('ref_axis',(0.,0.,1.));
#11236=DIRECTION('center_axis',(0.,0.,1.));
#11237=DIRECTION('ref_axis',(-0.707106781186535,0.70710678118656,0.));
#11238=DIRECTION('',(0.,0.,1.));
#11239=DIRECTION('center_axis',(-0.816496580927727,0.40824829046386,-0.408248290463864));
#11240=DIRECTION('ref_axis',(-0.577350269189631,-0.577350269189623,0.577350269189623));
#11241=DIRECTION('center_axis',(0.,0.,1.));
#11242=DIRECTION('ref_axis',(0.,-1.,0.));
#11243=DIRECTION('center_axis',(-1.,0.,0.));
#11244=DIRECTION('ref_axis',(0.,0.,1.));
#11245=DIRECTION('center_axis',(0.,-1.,0.));
#11246=DIRECTION('ref_axis',(-1.,0.,0.));
#11247=DIRECTION('center_axis',(-1.,0.,0.));
#11248=DIRECTION('ref_axis',(0.,-0.707106781186551,0.707106781186544));
#11249=DIRECTION('',(-1.,0.,0.));
#11250=DIRECTION('center_axis',(0.,-1.,0.));
#11251=DIRECTION('ref_axis',(-0.707106781186544,0.,0.707106781186551));
#11252=DIRECTION('',(0.,1.,0.));
#11253=DIRECTION('',(0.,-1.,0.));
#11254=DIRECTION('center_axis',(-0.816496580927733,0.408248290463859,-0.408248290463852));
#11255=DIRECTION('ref_axis',(-0.577350269189616,-0.577350269189631,0.577350269189631));
#11256=DIRECTION('center_axis',(-1.,-1.77635683940023E-14,0.));
#11257=DIRECTION('ref_axis',(0.,0.,1.));
#11258=DIRECTION('center_axis',(0.,-1.,0.));
#11259=DIRECTION('ref_axis',(-1.,0.,0.));
#11260=DIRECTION('center_axis',(4.44089209850056E-15,0.,1.));
#11261=DIRECTION('ref_axis',(0.,-1.,0.));
#11262=DIRECTION('center_axis',(0.,-1.,0.));
#11263=DIRECTION('ref_axis',(-0.707106781186541,0.,0.707106781186554));
#11264=DIRECTION('',(0.,1.,0.));
#11265=DIRECTION('',(0.,-1.,0.));
#11266=DIRECTION('center_axis',(0.,0.,-1.));
#11267=DIRECTION('ref_axis',(-0.707106781186548,-0.707106781186548,0.));
#11268=DIRECTION('',(0.,0.,-1.));
#11269=DIRECTION('center_axis',(0.,1.,0.));
#11270=DIRECTION('ref_axis',(0.,0.,1.));
#11271=DIRECTION('center_axis',(-1.,0.,0.));
#11272=DIRECTION('ref_axis',(0.,0.,1.));
#11273=DIRECTION('center_axis',(0.,-1.,0.));
#11274=DIRECTION('ref_axis',(1.,0.,0.));
#11275=DIRECTION('center_axis',(0.,0.,1.));
#11276=DIRECTION('ref_axis',(0.,1.,0.));
#11277=DIRECTION('center_axis',(0.408248290463856,0.408248290463856,-0.816496580927733));
#11278=DIRECTION('ref_axis',(0.577350269189645,0.577350269189616,0.577350269189616));
#11279=DIRECTION('center_axis',(0.,1.,0.));
#11280=DIRECTION('ref_axis',(1.,0.,0.));
#11281=DIRECTION('center_axis',(1.,1.77635683940023E-14,0.));
#11282=DIRECTION('ref_axis',(0.,0.,1.));
#11283=DIRECTION('center_axis',(0.,-1.,0.));
#11284=DIRECTION('ref_axis',(0.,0.,-1.));
#11285=DIRECTION('center_axis',(0.,0.,1.));
#11286=DIRECTION('ref_axis',(-1.,0.,0.));
#11287=DIRECTION('center_axis',(0.,1.,0.));
#11288=DIRECTION('ref_axis',(0.,0.,-1.));
#11289=DIRECTION('center_axis',(-1.,0.,0.));
#11290=DIRECTION('ref_axis',(0.,-1.,0.));
#11291=DIRECTION('center_axis',(0.,0.,-1.));
#11292=DIRECTION('ref_axis',(-0.707106781186541,-0.707106781186554,0.));
#11293=DIRECTION('',(0.,0.,-1.));
#11294=DIRECTION('center_axis',(0.,-1.,0.));
#11295=DIRECTION('ref_axis',(0.707106781186547,0.,-0.707106781186548));
#11296=DIRECTION('',(0.,1.,0.));
#11297=DIRECTION('',(0.,-1.,0.));
#11298=DIRECTION('center_axis',(-0.816496580927733,-0.408248290463852,0.40824829046386));
#11299=DIRECTION('ref_axis',(0.577350269189623,-0.577350269189623,0.577350269189631));
#11300=DIRECTION('center_axis',(1.,0.,0.));
#11301=DIRECTION('ref_axis',(0.,-1.,0.));
#11302=DIRECTION('center_axis',(0.,-1.,0.));
#11303=DIRECTION('ref_axis',(0.,0.,1.));
#11304=DIRECTION('center_axis',(0.,1.,0.));
#11305=DIRECTION('ref_axis',(0.,0.,1.));
#11306=DIRECTION('center_axis',(0.,0.,1.));
#11307=DIRECTION('ref_axis',(1.,0.,0.));
#11308=DIRECTION('center_axis',(0.,-1.,0.));
#11309=DIRECTION('ref_axis',(0.,0.,-1.));
#11310=DIRECTION('center_axis',(1.,0.,0.));
#11311=DIRECTION('ref_axis',(0.,1.,0.));
#11312=DIRECTION('center_axis',(0.,-1.,0.));
#11313=DIRECTION('ref_axis',(0.,0.,-1.));
#11314=DIRECTION('center_axis',(1.,0.,0.));
#11315=DIRECTION('ref_axis',(0.,0.,1.));
#11316=DIRECTION('center_axis',(0.,1.,0.));
#11317=DIRECTION('ref_axis',(-1.,0.,0.));
#11318=DIRECTION('center_axis',(0.,0.,1.));
#11319=DIRECTION('ref_axis',(0.,-1.,0.));
#11320=DIRECTION('center_axis',(-1.,0.,0.));
#11321=DIRECTION('ref_axis',(0.,-0.707106781186553,0.707106781186542));
#11322=DIRECTION('',(-1.,0.,0.));
#11323=DIRECTION('center_axis',(0.,-1.,0.));
#11324=DIRECTION('ref_axis',(-0.707106781186546,0.,-0.707106781186549));
#11325=DIRECTION('',(0.,1.,0.));
#11326=DIRECTION('',(0.,-1.,0.));
#11327=DIRECTION('center_axis',(-0.816496580927737,0.408248290463858,0.408248290463847));
#11328=DIRECTION('ref_axis',(0.577350269189605,0.577350269189647,0.577350269189626));
#11329=DIRECTION('center_axis',(0.,0.,1.));
#11330=DIRECTION('ref_axis',(0.,1.,0.));
#11331=DIRECTION('center_axis',(1.,1.77635683940023E-14,0.));
#11332=DIRECTION('ref_axis',(0.,0.,1.));
#11333=DIRECTION('center_axis',(0.,1.,0.));
#11334=DIRECTION('ref_axis',(1.,0.,0.));
#11335=DIRECTION('center_axis',(0.408248290463859,-0.408248290463859,-0.81649658092773));
#11336=DIRECTION('ref_axis',(-0.577350269189628,0.577350269189628,-0.577350269189622));
#11337=DIRECTION('center_axis',(0.,0.,-1.));
#11338=DIRECTION('ref_axis',(0.,1.,0.));
#11339=DIRECTION('center_axis',(-1.,0.,0.));
#11340=DIRECTION('ref_axis',(0.,0.,-1.));
#11341=DIRECTION('center_axis',(0.,1.,0.));
#11342=DIRECTION('ref_axis',(-1.,0.,0.));
#11343=DIRECTION('center_axis',(-1.,0.,0.));
#11344=DIRECTION('ref_axis',(0.,0.707106781186553,-0.707106781186543));
#11345=DIRECTION('',(-1.,0.,0.));
#11346=DIRECTION('center_axis',(-0.816496580927728,-0.408248290463861,0.408248290463861));
#11347=DIRECTION('ref_axis',(0.577350269189631,-0.577350269189623,0.577350269189623));
#11348=DIRECTION('center_axis',(1.,0.,-8.88178419700124E-15));
#11349=DIRECTION('ref_axis',(0.,-1.,0.));
#11350=DIRECTION('center_axis',(0.,0.,1.));
#11351=DIRECTION('ref_axis',(1.,0.,0.));
#11352=DIRECTION('center_axis',(0.,-1.,0.));
#11353=DIRECTION('ref_axis',(0.,0.,1.));
#11354=DIRECTION('center_axis',(0.,0.,1.));
#11355=DIRECTION('ref_axis',(0.707106781186541,-0.707106781186554,0.));
#11356=DIRECTION('',(0.,0.,1.));
#11357=DIRECTION('center_axis',(0.,-1.,0.));
#11358=DIRECTION('ref_axis',(0.707106781186544,0.,0.707106781186551));
#11359=DIRECTION('',(0.,1.,0.));
#11360=DIRECTION('',(0.,-1.,0.));
#11361=DIRECTION('center_axis',(-0.816496580927738,0.408248290463855,0.408248290463848));
#11362=DIRECTION('ref_axis',(-0.577350269189624,-0.577350269189624,-0.577350269189629));
#11363=DIRECTION('center_axis',(0.,-1.,0.));
#11364=DIRECTION('ref_axis',(0.,0.,-1.));
#11365=DIRECTION('center_axis',(-1.,0.,1.77635683940025E-14));
#11366=DIRECTION('ref_axis',(0.,-1.,0.));
#11367=DIRECTION('center_axis',(0.,-1.,0.));
#11368=DIRECTION('ref_axis',(-0.70710678118654,0.,-0.707106781186555));
#11369=DIRECTION('',(0.,1.,0.));
#11370=DIRECTION('',(0.,-1.,0.));
#11371=DIRECTION('center_axis',(1.,0.,0.));
#11372=DIRECTION('ref_axis',(0.,-0.707106781186553,-0.707106781186543));
#11373=DIRECTION('',(1.,0.,0.));
#11374=DIRECTION('center_axis',(0.,1.,-3.55271367880045E-14));
#11375=DIRECTION('ref_axis',(0.,2.84217094304041E-14,1.));
#11376=DIRECTION('center_axis',(0.707106781186548,2.512147933894E-14,0.707106781186548));
#11377=DIRECTION('ref_axis',(0.707106781186548,0.,-0.707106781186548));
#11378=DIRECTION('center_axis',(0.,-1.,0.));
#11379=DIRECTION('ref_axis',(0.,0.,-1.));
#11380=DIRECTION('center_axis',(1.,0.,0.));
#11381=DIRECTION('ref_axis',(0.,1.,0.));
#11382=DIRECTION('center_axis',(-0.816496580927733,-0.408248290463852,-0.40824829046386));
#11383=DIRECTION('ref_axis',(-0.577350269189623,0.577350269189623,0.577350269189631));
#11384=DIRECTION('center_axis',(-1.,0.,0.));
#11385=DIRECTION('ref_axis',(0.,1.,0.));
#11386=DIRECTION('center_axis',(0.,1.,0.));
#11387=DIRECTION('ref_axis',(0.,0.,1.));
#11388=DIRECTION('center_axis',(0.,0.,1.));
#11389=DIRECTION('ref_axis',(-0.707106781186548,0.707106781186548,0.));
#11390=DIRECTION('',(0.,0.,1.));
#11391=DIRECTION('center_axis',(0.,1.,0.));
#11392=DIRECTION('ref_axis',(0.,0.,1.));
#11393=DIRECTION('center_axis',(1.,0.,0.));
#11394=DIRECTION('ref_axis',(0.,0.,1.));
#11395=DIRECTION('center_axis',(0.,1.,0.));
#11396=DIRECTION('ref_axis',(-0.707106781186548,0.,0.707106781186548));
#11397=DIRECTION('center_axis',(0.707106781186554,0.,0.707106781186541));
#11398=DIRECTION('ref_axis',(0.,-1.,0.));
#11399=DIRECTION('center_axis',(-0.408248290463856,-0.408248290463856,-0.816496580927733));
#11400=DIRECTION('ref_axis',(-0.577350269189645,-0.577350269189616,0.577350269189616));
#11401=DIRECTION('center_axis',(0.,-1.,0.));
#11402=DIRECTION('ref_axis',(-1.,0.,0.));
#11403=DIRECTION('center_axis',(0.,0.,1.));
#11404=DIRECTION('ref_axis',(0.,-1.,0.));
#11405=DIRECTION('center_axis',(-1.,-1.77635683940023E-14,0.));
#11406=DIRECTION('ref_axis',(0.,0.,1.));
#11407=DIRECTION('center_axis',(0.,0.,1.));
#11408=DIRECTION('ref_axis',(-0.707106781186548,-0.707106781186548,0.));
#11409=DIRECTION('center_axis',(-0.827465426020369,0.538877990790914,0.157833709270475));
#11410=DIRECTION('ref_axis',(0.561516668266342,0.794104487760818,0.232587819494476));
#11411=DIRECTION('center_axis',(0.,1.,0.));
#11412=DIRECTION('ref_axis',(0.707106781186548,0.,-0.707106781186548));
#11413=DIRECTION('center_axis',(0.707106781186548,0.,0.707106781186548));
#11414=DIRECTION('ref_axis',(0.,1.,0.));
#11415=DIRECTION('center_axis',(1.,0.,0.));
#11416=DIRECTION('ref_axis',(0.,0.,1.));
#11417=DIRECTION('center_axis',(-0.707106781186548,0.,-0.707106781186548));
#11418=DIRECTION('ref_axis',(0.499999999999996,0.707106781186553,-0.499999999999996));
#11419=DIRECTION('',(-0.707106781186548,0.,-0.707106781186548));
#11420=DIRECTION('center_axis',(-1.,0.,0.));
#11421=DIRECTION('ref_axis',(0.,0.707106781186551,0.707106781186544));
#11422=DIRECTION('',(1.,0.,0.));
#11423=DIRECTION('center_axis',(-0.827465426020366,-0.538877990790921,0.15783370927047));
#11424=DIRECTION('ref_axis',(0.561516668266338,-0.794104487760823,0.23258781949447));
#11425=DIRECTION('center_axis',(0.707106781186548,0.,0.707106781186548));
#11426=DIRECTION('ref_axis',(0.707106781186548,0.,-0.707106781186548));
#11427=DIRECTION('center_axis',(0.,-1.,0.));
#11428=DIRECTION('ref_axis',(0.,0.,1.));
#11429=DIRECTION('center_axis',(1.,0.,0.));
#11430=DIRECTION('ref_axis',(0.,-1.,0.));
#11431=DIRECTION('center_axis',(0.,1.,0.));
#11432=DIRECTION('ref_axis',(0.923879532511288,0.,0.382683432365088));
#11433=DIRECTION('',(0.,-1.,0.));
#11434=DIRECTION('',(0.,1.,0.));
#11435=DIRECTION('center_axis',(1.,0.,0.));
#11436=DIRECTION('ref_axis',(0.,-0.707106781186551,0.707106781186544));
#11437=DIRECTION('',(-1.,0.,0.));
#11438=DIRECTION('center_axis',(0.707106781186548,0.,0.707106781186548));
#11439=DIRECTION('ref_axis',(0.499999999999996,-0.707106781186553,-0.499999999999996));
#11440=DIRECTION('',(0.707106781186548,0.,0.707106781186548));
#11441=DIRECTION('center_axis',(0.,-1.,0.));
#11442=DIRECTION('ref_axis',(-0.707106781186538,0.,0.707106781186557));
#11443=DIRECTION('',(0.,1.,0.));
#11444=DIRECTION('center_axis',(-1.,0.,0.));
#11445=DIRECTION('ref_axis',(0.,-0.707106781186551,0.707106781186544));
#11446=DIRECTION('',(-1.,0.,0.));
#11447=DIRECTION('center_axis',(0.,-1.,0.));
#11448=DIRECTION('ref_axis',(-0.923879532511288,0.,-0.382683432365088));
#11449=DIRECTION('',(0.,1.,0.));
#11450=DIRECTION('',(0.,-1.,0.));
#11451=DIRECTION('center_axis',(1.,0.,0.));
#11452=DIRECTION('ref_axis',(0.,0.707106781186551,0.707106781186544));
#11453=DIRECTION('',(1.,0.,0.));
#11454=DIRECTION('center_axis',(0.,0.,-1.));
#11455=DIRECTION('ref_axis',(0.707106781186548,0.707106781186548,0.));
#11456=DIRECTION('',(0.,0.,-1.));
#11457=DIRECTION('center_axis',(1.,0.,0.));
#11458=DIRECTION('ref_axis',(0.,0.707106781186553,0.707106781186542));
#11459=DIRECTION('',(1.,0.,0.));
#11460=DIRECTION('center_axis',(0.,1.,0.));
#11461=DIRECTION('ref_axis',(0.707106781186538,0.,0.707106781186557));
#11462=DIRECTION('',(0.,-1.,0.));
#11463=DIRECTION('center_axis',(1.,0.,0.));
#11464=DIRECTION('ref_axis',(0.,-0.707106781186551,0.707106781186544));
#11465=DIRECTION('',(-1.,0.,0.));
#11466=DIRECTION('center_axis',(-1.,0.,0.));
#11467=DIRECTION('ref_axis',(0.,0.707106781186551,0.707106781186544));
#11468=DIRECTION('',(1.,0.,0.));
#11469=DIRECTION('center_axis',(0.,0.,1.));
#11470=DIRECTION('ref_axis',(-0.707106781186541,0.707106781186554,0.));
#11471=DIRECTION('',(0.,0.,1.));
#11472=DIRECTION('center_axis',(1.,0.,0.));
#11473=DIRECTION('ref_axis',(0.,0.707106781186551,0.707106781186544));
#11474=DIRECTION('',(1.,0.,0.));
#11475=DIRECTION('center_axis',(0.,-1.,0.));
#11476=DIRECTION('ref_axis',(0.707106781186538,0.,-0.707106781186557));
#11477=DIRECTION('',(0.,1.,0.));
#11478=DIRECTION('',(0.,-1.,0.));
#11479=DIRECTION('center_axis',(0.,0.,1.));
#11480=DIRECTION('ref_axis',(1.,0.,0.));
#11481=DIRECTION('center_axis',(1.,0.,0.));
#11482=DIRECTION('ref_axis',(0.,0.,1.));
#11483=DIRECTION('center_axis',(0.,0.,-1.));
#11484=DIRECTION('ref_axis',(1.,0.,0.));
#11485=DIRECTION('center_axis',(1.,0.,0.));
#11486=DIRECTION('ref_axis',(0.,0.,1.));
#11487=DIRECTION('center_axis',(0.,0.,-1.));
#11488=DIRECTION('ref_axis',(1.,0.,0.));
#11489=DIRECTION('center_axis',(-1.,0.,0.));
#11490=DIRECTION('ref_axis',(0.,0.,-1.));
#11491=DIRECTION('center_axis',(0.,0.,-1.));
#11492=DIRECTION('ref_axis',(1.,0.,0.));
#11493=DIRECTION('center_axis',(-1.,0.,0.));
#11494=DIRECTION('ref_axis',(0.,-1.,0.));
#11495=DIRECTION('center_axis',(-0.707106781186548,0.,0.707106781186548));
#11496=DIRECTION('ref_axis',(-0.707106781186548,0.,-0.707106781186548));
#11497=DIRECTION('center_axis',(0.,0.,1.));
#11498=DIRECTION('ref_axis',(1.,0.,0.));
#11499=DIRECTION('center_axis',(0.,0.,1.));
#11500=DIRECTION('ref_axis',(1.,0.,0.));
#14288=CARTESIAN_POINT('',(0.,0.,0.));
#14289=CARTESIAN_POINT('Origin',(65.,0.,6.28953555269655));
#14290=CARTESIAN_POINT('',(64.5,-90.,6.28953555269655));
#14291=CARTESIAN_POINT('',(65.,-89.5,6.28953555269655));
#14292=CARTESIAN_POINT('Origin',(64.5,-89.5,6.28953555269655));
#14293=CARTESIAN_POINT('',(62.,-90.,6.28953555269655));
#14294=CARTESIAN_POINT('',(0.,-90.,6.28953555269655));
#14295=CARTESIAN_POINT('',(62.,90.,6.28953555269655));
#14296=CARTESIAN_POINT('',(62.,0.,6.28953555269655));
#14297=CARTESIAN_POINT('',(64.5,90.,6.28953555269655));
#14298=CARTESIAN_POINT('',(65.,90.,6.28953555269655));
#14299=CARTESIAN_POINT('',(65.,89.5,6.28953555269655));
#14300=CARTESIAN_POINT('Origin',(64.5,89.5,6.28953555269655));
#14301=CARTESIAN_POINT('',(65.,-45.,6.28953555269655));
#14302=CARTESIAN_POINT('Origin',(62.,0.,2.78953555269655));
#14303=CARTESIAN_POINT('',(65.,-89.5,2.78953555269655));
#14304=CARTESIAN_POINT('',(64.5,-90.,2.78953555269655));
#14305=CARTESIAN_POINT('Origin',(64.5,-89.5,2.78953555269655));
#14306=CARTESIAN_POINT('',(65.,89.5,2.78953555269655));
#14307=CARTESIAN_POINT('',(65.,-45.,2.78953555269655));
#14308=CARTESIAN_POINT('',(64.5,90.,2.78953555269655));
#14309=CARTESIAN_POINT('Origin',(64.5,89.5,2.78953555269655));
#14310=CARTESIAN_POINT('',(62.,90.,2.78953555269655));
#14311=CARTESIAN_POINT('',(63.5,90.,2.78953555269655));
#14312=CARTESIAN_POINT('',(62.,-90.,2.78953555269655));
#14313=CARTESIAN_POINT('',(62.,0.,2.78953555269655));
#14314=CARTESIAN_POINT('',(-1.5,-90.,2.78953555269655));
#14315=CARTESIAN_POINT('Origin',(62.,0.,6.28953555269655));
#14316=CARTESIAN_POINT('',(62.,90.,3.14476777634828));
#14317=CARTESIAN_POINT('',(62.,-90.,3.14476777634828));
#14318=CARTESIAN_POINT('Origin',(64.5,-89.5,0.));
#14319=CARTESIAN_POINT('',(64.5,-90.,0.5));
#14320=CARTESIAN_POINT('',(64.5,-90.,0.));
#14321=CARTESIAN_POINT('',(65.,-89.5,0.));
#14322=CARTESIAN_POINT('Origin',(64.5,-89.5,0.5));
#14323=CARTESIAN_POINT('',(65.,-89.5,0.));
#14324=CARTESIAN_POINT('Origin',(64.5,-89.5,0.));
#14325=CARTESIAN_POINT('',(65.,-89.5,19.5));
#14326=CARTESIAN_POINT('',(65.,-89.5,0.));
#14327=CARTESIAN_POINT('',(64.5,-90.,19.5));
#14328=CARTESIAN_POINT('Origin',(64.5,-89.5,19.5));
#14329=CARTESIAN_POINT('',(64.5,-90.,0.));
#14330=CARTESIAN_POINT('Origin',(65.,-90.,0.));
#14331=CARTESIAN_POINT('',(65.,89.5,0.));
#14332=CARTESIAN_POINT('',(65.,-90.,0.));
#14333=CARTESIAN_POINT('',(65.,89.5,0.));
#14334=CARTESIAN_POINT('Origin',(65.,-90.,0.));
#14335=CARTESIAN_POINT('',(65.,89.5,19.5));
#14336=CARTESIAN_POINT('',(65.,89.5,0.));
#14337=CARTESIAN_POINT('',(65.,-45.,19.5));
#14338=CARTESIAN_POINT('Origin',(64.5,89.5,0.));
#14339=CARTESIAN_POINT('',(64.5,90.,0.5));
#14340=CARTESIAN_POINT('Origin',(64.5,89.5,0.5));
#14341=CARTESIAN_POINT('',(64.5,90.,0.));
#14342=CARTESIAN_POINT('Origin',(64.5,89.5,0.));
#14343=CARTESIAN_POINT('',(64.5,90.,19.5));
#14344=CARTESIAN_POINT('',(64.5,90.,0.));
#14345=CARTESIAN_POINT('Origin',(64.5,89.5,19.5));
#14346=CARTESIAN_POINT('Origin',(65.,90.,0.));
#14347=CARTESIAN_POINT('',(-64.5,90.,0.5));
#14348=CARTESIAN_POINT('',(32.5,90.,0.5));
#14349=CARTESIAN_POINT('',(-64.5,90.,2.78953555269655));
#14350=CARTESIAN_POINT('',(-64.5,90.,0.));
#14351=CARTESIAN_POINT('',(-62.,90.,2.78953555269655));
#14352=CARTESIAN_POINT('',(1.5,90.,2.78953555269655));
#14353=CARTESIAN_POINT('',(-62.,90.,6.28953555269655));
#14354=CARTESIAN_POINT('',(-62.,90.,3.14476777634828));
#14355=CARTESIAN_POINT('',(-64.5,90.,6.28953555269655));
#14356=CARTESIAN_POINT('',(0.,90.,6.28953555269655));
#14357=CARTESIAN_POINT('',(-64.5,90.,19.5));
#14358=CARTESIAN_POINT('',(-64.5,90.,0.));
#14359=CARTESIAN_POINT('',(-23.0395928638606,90.,19.5));
#14360=CARTESIAN_POINT('',(32.5,90.,19.5));
#14361=CARTESIAN_POINT('',(-25.6346603396366,90.,16.904932524224));
#14362=CARTESIAN_POINT('',(-5.47791795259883,90.,37.0616749112618));
#14363=CARTESIAN_POINT('',(-24.92755355845,90.,15.1978257430375));
#14364=CARTESIAN_POINT('Origin',(-24.92755355845,90.,16.1978257430375));
#14365=CARTESIAN_POINT('',(-19.5453000725091,90.,15.1978257430375));
#14366=CARTESIAN_POINT('',(19.4326698301817,90.,15.1978257430375));
#14367=CARTESIAN_POINT('',(-19.5453000725091,90.,4.19782574303749));
#14368=CARTESIAN_POINT('',(-19.5453000725091,90.,7.84891287151875));
#14369=CARTESIAN_POINT('',(-18.545300072509,90.,3.19782574303749));
#14370=CARTESIAN_POINT('Origin',(-18.545300072509,90.,4.19782574303749));
#14371=CARTESIAN_POINT('',(21.0741207385024,90.,3.19782574303749));
#14372=CARTESIAN_POINT('',(22.9773499637455,90.,3.19782574303749));
#14373=CARTESIAN_POINT('',(22.0741207385024,90.,4.19782574303749));
#14374=CARTESIAN_POINT('Origin',(21.0741207385024,90.,4.19782574303749));
#14375=CARTESIAN_POINT('',(22.0741207385024,90.,15.1978257430375));
#14376=CARTESIAN_POINT('',(22.0741207385024,90.,1.84891287151875));
#14377=CARTESIAN_POINT('',(44.3272645584125,90.,15.1978257430375));
#14378=CARTESIAN_POINT('',(43.2870603692512,90.,15.1978257430375));
#14379=CARTESIAN_POINT('',(45.3272645584125,90.,16.1978257430375));
#14380=CARTESIAN_POINT('Origin',(44.3272645584125,90.,16.1978257430375));
#14381=CARTESIAN_POINT('',(45.3272645584125,90.,19.5));
#14382=CARTESIAN_POINT('',(45.3272645584125,90.,7.84891287151875));
#14383=CARTESIAN_POINT('',(32.5,90.,19.5));
#14384=CARTESIAN_POINT('Origin',(-65.,0.,6.28953555269655));
#14385=CARTESIAN_POINT('',(-65.,89.5,6.28953555269655));
#14386=CARTESIAN_POINT('Origin',(-64.5,89.5,6.28953555269655));
#14387=CARTESIAN_POINT('',(-62.,-90.,6.28953555269655));
#14388=CARTESIAN_POINT('',(-62.,0.,6.28953555269655));
#14389=CARTESIAN_POINT('',(-64.5,-90.,6.28953555269655));
#14390=CARTESIAN_POINT('',(-65.,-90.,6.28953555269655));
#14391=CARTESIAN_POINT('',(-65.,-89.5,6.28953555269655));
#14392=CARTESIAN_POINT('Origin',(-64.5,-89.5,6.28953555269655));
#14393=CARTESIAN_POINT('',(-65.,45.,6.28953555269655));
#14394=CARTESIAN_POINT('Origin',(-62.,0.,2.78953555269655));
#14395=CARTESIAN_POINT('',(-65.,89.5,2.78953555269655));
#14396=CARTESIAN_POINT('Origin',(-64.5,89.5,2.78953555269655));
#14397=CARTESIAN_POINT('',(-65.,-89.5,2.78953555269655));
#14398=CARTESIAN_POINT('',(-65.,45.,2.78953555269655));
#14399=CARTESIAN_POINT('',(-64.5,-90.,2.78953555269655));
#14400=CARTESIAN_POINT('Origin',(-64.5,-89.5,2.78953555269655));
#14401=CARTESIAN_POINT('',(-62.,-90.,2.78953555269655));
#14402=CARTESIAN_POINT('',(-63.5,-90.,2.78953555269655));
#14403=CARTESIAN_POINT('',(-62.,0.,2.78953555269655));
#14404=CARTESIAN_POINT('Origin',(-62.,0.,6.28953555269655));
#14405=CARTESIAN_POINT('',(-62.,-90.,3.14476777634828));
#14406=CARTESIAN_POINT('Origin',(-64.5,89.5,0.));
#14407=CARTESIAN_POINT('',(-65.,89.5,19.5));
#14408=CARTESIAN_POINT('',(-65.,89.5,0.));
#14409=CARTESIAN_POINT('Origin',(-64.5,89.5,19.5));
#14410=CARTESIAN_POINT('Origin',(-65.,-90.,0.));
#14411=CARTESIAN_POINT('',(45.3272645584125,-90.,19.5));
#14412=CARTESIAN_POINT('',(-32.5,-90.,19.5));
#14413=CARTESIAN_POINT('',(45.3272645584125,-90.,16.1978257430375));
#14414=CARTESIAN_POINT('',(45.3272645584125,-90.,7.84891287151875));
#14415=CARTESIAN_POINT('',(44.3272645584124,-90.,15.1978257430375));
#14416=CARTESIAN_POINT('Origin',(44.3272645584124,-90.,16.1978257430375));
#14417=CARTESIAN_POINT('',(22.0741207385024,-90.,15.1978257430375));
#14418=CARTESIAN_POINT('',(-21.7129396307488,-90.,15.1978257430375));
#14419=CARTESIAN_POINT('',(22.0741207385024,-90.,4.19782574303749));
#14420=CARTESIAN_POINT('',(22.0741207385024,-90.,1.84891287151875));
#14421=CARTESIAN_POINT('',(21.0741207385024,-90.,3.19782574303749));
#14422=CARTESIAN_POINT('Origin',(21.0741207385024,-90.,4.19782574303749));
#14423=CARTESIAN_POINT('',(-18.545300072509,-90.,3.19782574303749));
#14424=CARTESIAN_POINT('',(-42.0226500362545,-90.,3.19782574303749));
#14425=CARTESIAN_POINT('',(-19.545300072509,-90.,4.19782574303749));
#14426=CARTESIAN_POINT('Origin',(-18.545300072509,-90.,4.19782574303749));
#14427=CARTESIAN_POINT('',(-19.545300072509,-90.,15.1978257430375));
#14428=CARTESIAN_POINT('',(-19.545300072509,-90.,7.84891287151875));
#14429=CARTESIAN_POINT('',(-24.92755355845,-90.,15.1978257430375));
#14430=CARTESIAN_POINT('',(-45.5673301698183,-90.,15.1978257430375));
#14431=CARTESIAN_POINT('',(-25.6346603396366,-90.,16.904932524224));
#14432=CARTESIAN_POINT('Origin',(-24.92755355845,-90.,16.1978257430375));
#14433=CARTESIAN_POINT('',(-23.0395928638606,-90.,19.5));
#14434=CARTESIAN_POINT('',(-37.9779179525988,-90.,4.56167491126179));
#14435=CARTESIAN_POINT('',(-64.5,-90.,19.5));
#14436=CARTESIAN_POINT('',(-32.5,-90.,19.5));
#14437=CARTESIAN_POINT('',(-64.5,-90.,0.));
#14438=CARTESIAN_POINT('',(-64.5,-90.,0.5));
#14439=CARTESIAN_POINT('',(-64.5,-90.,0.));
#14440=CARTESIAN_POINT('',(-32.5,-90.,0.5));
#14441=CARTESIAN_POINT('Origin',(-65.,90.,0.));
#14442=CARTESIAN_POINT('',(-65.,-89.5,19.5));
#14443=CARTESIAN_POINT('',(-65.,-89.5,0.));
#14444=CARTESIAN_POINT('',(-65.,45.,19.5));
#14445=CARTESIAN_POINT('Origin',(-64.5,-89.5,0.));
#14446=CARTESIAN_POINT('',(-65.,-89.5,0.5));
#14447=CARTESIAN_POINT('',(-65.,-89.5,0.));
#14448=CARTESIAN_POINT('Origin',(-64.5,-89.5,0.5));
#14449=CARTESIAN_POINT('Origin',(44.3272645584125,89.5,16.1978257430375));
#14450=CARTESIAN_POINT('',(44.3272645584125,89.5,15.6978257430375));
#14451=CARTESIAN_POINT('Origin',(44.3272645584125,89.5,15.1978257430375));
#14452=CARTESIAN_POINT('',(44.8272645584125,89.5,16.1978257430375));
#14453=CARTESIAN_POINT('Origin',(44.3272645584125,89.5,16.1978257430375));
#14454=CARTESIAN_POINT('Origin',(45.3272645584125,89.5,16.1978257430375));
#14455=CARTESIAN_POINT('Origin',(44.3272645584124,-89.5,16.1978257430375));
#14456=CARTESIAN_POINT('',(44.8272645584125,-89.5,16.1978257430375));
#14457=CARTESIAN_POINT('Origin',(45.3272645584125,-89.5,16.1978257430375));
#14458=CARTESIAN_POINT('',(44.3272645584124,-89.5,15.6978257430375));
#14459=CARTESIAN_POINT('Origin',(44.3272645584125,-89.5,16.1978257430375));
#14460=CARTESIAN_POINT('Origin',(44.3272645584124,-89.5,15.1978257430375));
#14461=CARTESIAN_POINT('Origin',(22.0741207385024,89.5,15.1978257430375));
#14462=CARTESIAN_POINT('',(22.0741207385024,89.5,15.6978257430375));
#14463=CARTESIAN_POINT('Origin',(22.0741207385024,89.5,15.1978257430375));
#14464=CARTESIAN_POINT('',(21.5741207385024,89.5,15.1978257430375));
#14465=CARTESIAN_POINT('Origin',(22.0741207385024,89.5,15.1978257430375));
#14466=CARTESIAN_POINT('Origin',(22.0741207385024,89.5,15.1978257430375));
#14467=CARTESIAN_POINT('Origin',(45.3272645584125,89.5,19.5));
#14468=CARTESIAN_POINT('',(45.3272645584125,89.5,20.));
#14469=CARTESIAN_POINT('Origin',(45.3272645584125,89.5,19.5));
#14470=CARTESIAN_POINT('',(44.8272645584125,89.5,19.5));
#14471=CARTESIAN_POINT('Origin',(45.3272645584125,89.5,19.5));
#14472=CARTESIAN_POINT('Origin',(45.3272645584125,89.5,19.5));
#14473=CARTESIAN_POINT('Origin',(45.3272645584125,89.5,7.84891287151875));
#14474=CARTESIAN_POINT('',(44.8272645584125,89.5,7.84891287151875));
#14475=CARTESIAN_POINT('Origin',(22.0741207385024,-89.5,15.1978257430375));
#14476=CARTESIAN_POINT('',(21.5741207385024,-89.5,15.1978257430375));
#14477=CARTESIAN_POINT('Origin',(22.0741207385024,-89.5,15.1978257430375));
#14478=CARTESIAN_POINT('',(22.0741207385024,-89.5,15.6978257430375));
#14479=CARTESIAN_POINT('Origin',(22.0741207385024,-89.5,15.1978257430375));
#14480=CARTESIAN_POINT('Origin',(22.0741207385024,-89.5,15.1978257430375));
#14481=CARTESIAN_POINT('Origin',(-21.7129396307488,-89.5,15.1978257430375));
#14482=CARTESIAN_POINT('',(-21.7129396307488,-89.5,15.6978257430375));
#14483=CARTESIAN_POINT('Origin',(22.0741207385024,-90.,15.1978257430375));
#14484=CARTESIAN_POINT('',(22.0741207385024,-90.,15.6978257430375));
#14485=CARTESIAN_POINT('',(21.5741207385024,-90.,15.1978257430375));
#14486=CARTESIAN_POINT('Origin',(45.3272645584125,-89.5,19.5));
#14487=CARTESIAN_POINT('',(45.3272645584125,-89.5,20.));
#14488=CARTESIAN_POINT('Origin',(45.3272645584125,-89.5,19.5));
#14489=CARTESIAN_POINT('',(44.8272645584125,-89.5,19.5));
#14490=CARTESIAN_POINT('Origin',(45.3272645584125,-89.5,19.5));
#14491=CARTESIAN_POINT('Origin',(45.3272645584125,-89.5,19.5));
#14492=CARTESIAN_POINT('Origin',(45.3272645584125,-45.,19.5));
#14493=CARTESIAN_POINT('',(45.3272645584125,-45.,20.));
#14494=CARTESIAN_POINT('',(44.8272645584125,-45.,19.5));
#14495=CARTESIAN_POINT('Origin',(45.3272645584125,-89.5,7.84891287151875));
#14496=CARTESIAN_POINT('',(44.8272645584125,-89.5,7.84891287151875));
#14497=CARTESIAN_POINT('Origin',(21.0741207385024,89.5,4.19782574303749));
#14498=CARTESIAN_POINT('',(21.0741207385024,89.5,3.69782574303749));
#14499=CARTESIAN_POINT('Origin',(21.0741207385024,89.5,3.19782574303749));
#14500=CARTESIAN_POINT('',(21.5741207385024,89.5,4.19782574303749));
#14501=CARTESIAN_POINT('Origin',(21.0741207385024,89.5,4.19782574303749));
#14502=CARTESIAN_POINT('Origin',(22.0741207385024,89.5,4.19782574303749));
#14503=CARTESIAN_POINT('Origin',(64.5,89.5,19.5));
#14504=CARTESIAN_POINT('',(64.5,89.5,20.));
#14505=CARTESIAN_POINT('Origin',(64.5,89.5,19.5));
#14506=CARTESIAN_POINT('Origin',(64.5,89.5,19.5));
#14507=CARTESIAN_POINT('Origin',(21.0741207385024,-89.5,4.19782574303749));
#14508=CARTESIAN_POINT('',(21.5741207385024,-89.5,4.19782574303749));
#14509=CARTESIAN_POINT('Origin',(22.0741207385024,-89.5,4.19782574303749));
#14510=CARTESIAN_POINT('',(21.0741207385024,-89.5,3.69782574303749));
#14511=CARTESIAN_POINT('Origin',(21.0741207385024,-89.5,4.19782574303749));
#14512=CARTESIAN_POINT('Origin',(21.0741207385024,-89.5,3.19782574303749));
#14513=CARTESIAN_POINT('Origin',(22.0741207385024,-89.5,1.84891287151875));
#14514=CARTESIAN_POINT('',(21.5741207385024,-89.5,1.84891287151875));
#14515=CARTESIAN_POINT('Origin',(21.0741207385024,-90.,4.19782574303749));
#14516=CARTESIAN_POINT('',(21.5741207385024,-90.,4.19782574303749));
#14517=CARTESIAN_POINT('',(21.0741207385024,-90.,3.69782574303749));
#14518=CARTESIAN_POINT('Origin',(64.5,-89.5,19.5));
#14519=CARTESIAN_POINT('',(64.5,-89.5,20.));
#14520=CARTESIAN_POINT('Origin',(64.5,-89.5,19.5));
#14521=CARTESIAN_POINT('Origin',(64.5,-89.5,19.5));
#14522=CARTESIAN_POINT('Origin',(-18.545300072509,89.5,4.19782574303749));
#14523=CARTESIAN_POINT('',(-19.045300072509,89.5,4.19782574303749));
#14524=CARTESIAN_POINT('Origin',(-19.5453000725091,89.5,4.19782574303749));
#14525=CARTESIAN_POINT('',(-18.545300072509,89.5,3.69782574303749));
#14526=CARTESIAN_POINT('Origin',(-18.545300072509,89.5,4.19782574303749));
#14527=CARTESIAN_POINT('Origin',(-18.545300072509,89.5,3.19782574303749));
#14528=CARTESIAN_POINT('Origin',(-18.545300072509,-89.5,4.19782574303749));
#14529=CARTESIAN_POINT('',(-18.545300072509,-89.5,3.69782574303749));
#14530=CARTESIAN_POINT('Origin',(-18.545300072509,-89.5,3.19782574303749));
#14531=CARTESIAN_POINT('',(-19.045300072509,-89.5,4.19782574303749));
#14532=CARTESIAN_POINT('Origin',(-18.545300072509,-89.5,4.19782574303749));
#14533=CARTESIAN_POINT('Origin',(-19.545300072509,-89.5,4.19782574303749));
#14534=CARTESIAN_POINT('Origin',(-42.0226500362545,-89.5,3.19782574303749));
#14535=CARTESIAN_POINT('',(-42.0226500362545,-89.5,3.69782574303749));
#14536=CARTESIAN_POINT('Origin',(-18.545300072509,-90.,4.19782574303749));
#14537=CARTESIAN_POINT('',(-18.545300072509,-90.,3.69782574303749));
#14538=CARTESIAN_POINT('',(-19.045300072509,-90.,4.19782574303749));
#14539=CARTESIAN_POINT('Origin',(-19.545300072509,89.5,15.1978257430375));
#14540=CARTESIAN_POINT('',(-19.045300072509,89.5,15.1978257430375));
#14541=CARTESIAN_POINT('Origin',(-19.5453000725091,89.5,15.1978257430375));
#14542=CARTESIAN_POINT('',(-19.545300072509,89.5,15.6978257430375));
#14543=CARTESIAN_POINT('Origin',(-19.545300072509,89.5,15.1978257430375));
#14544=CARTESIAN_POINT('Origin',(-19.545300072509,89.5,15.1978257430375));
#14545=CARTESIAN_POINT('Origin',(-64.5,89.5,0.5));
#14546=CARTESIAN_POINT('',(-65.,89.5,0.5));
#14547=CARTESIAN_POINT('Origin',(-64.5,89.5,0.5));
#14548=CARTESIAN_POINT('',(-64.5,89.5,0.));
#14549=CARTESIAN_POINT('Origin',(-64.5,89.5,0.5));
#14550=CARTESIAN_POINT('Origin',(-64.5,89.5,0.5));
#14551=CARTESIAN_POINT('Origin',(32.5,89.5,0.5));
#14552=CARTESIAN_POINT('',(32.5,89.5,0.));
#14553=CARTESIAN_POINT('Origin',(-19.545300072509,-89.5,15.1978257430375));
#14554=CARTESIAN_POINT('',(-19.545300072509,-89.5,15.6978257430375));
#14555=CARTESIAN_POINT('Origin',(-19.545300072509,-89.5,15.1978257430375));
#14556=CARTESIAN_POINT('',(-19.045300072509,-89.5,15.1978257430375));
#14557=CARTESIAN_POINT('Origin',(-19.545300072509,-89.5,15.1978257430375));
#14558=CARTESIAN_POINT('Origin',(-19.545300072509,-89.5,15.1978257430375));
#14559=CARTESIAN_POINT('Origin',(-19.545300072509,-89.5,7.84891287151875));
#14560=CARTESIAN_POINT('',(-19.045300072509,-89.5,7.84891287151875));
#14561=CARTESIAN_POINT('Origin',(-19.545300072509,-90.,15.1978257430375));
#14562=CARTESIAN_POINT('',(-19.045300072509,-90.,15.1978257430375));
#14563=CARTESIAN_POINT('',(-19.545300072509,-90.,15.6978257430375));
#14564=CARTESIAN_POINT('Origin',(-64.5,-89.5,0.5));
#14565=CARTESIAN_POINT('',(-64.5,-89.5,0.));
#14566=CARTESIAN_POINT('Origin',(-64.5,-89.5,0.5));
#14567=CARTESIAN_POINT('Origin',(-64.5,-89.5,0.5));
#14568=CARTESIAN_POINT('Origin',(-64.5,45.,0.5));
#14569=CARTESIAN_POINT('',(-65.,45.,0.5));
#14570=CARTESIAN_POINT('',(-64.5,45.,0.));
#14571=CARTESIAN_POINT('Origin',(-32.5,-89.5,0.5));
#14572=CARTESIAN_POINT('',(-32.5,-89.5,0.));
#14573=CARTESIAN_POINT('Origin',(-24.92755355845,89.5,16.1978257430375));
#14574=CARTESIAN_POINT('',(-25.2811069490433,89.5,16.5513791336308));
#14575=CARTESIAN_POINT('Origin',(-25.6346603396366,89.5,16.904932524224));
#14576=CARTESIAN_POINT('',(-24.92755355845,89.5,15.6978257430375));
#14577=CARTESIAN_POINT('Origin',(-24.92755355845,89.5,16.1978257430375));
#14578=CARTESIAN_POINT('Origin',(-24.92755355845,89.5,15.1978257430375));
#14579=CARTESIAN_POINT('Origin',(-64.5,89.5,19.5));
#14580=CARTESIAN_POINT('',(-64.5,89.5,20.));
#14581=CARTESIAN_POINT('Origin',(-64.5,89.5,19.5));
#14582=CARTESIAN_POINT('Origin',(-64.5,89.5,19.5));
#14583=CARTESIAN_POINT('Origin',(-64.5,89.5,0.));
#14584=CARTESIAN_POINT('',(-65.,89.5,0.));
#14585=CARTESIAN_POINT('Origin',(-24.92755355845,-89.5,16.1978257430375));
#14586=CARTESIAN_POINT('',(-24.92755355845,-89.5,15.6978257430375));
#14587=CARTESIAN_POINT('Origin',(-24.92755355845,-89.5,15.1978257430375));
#14588=CARTESIAN_POINT('',(-25.2811069490433,-89.5,16.5513791336308));
#14589=CARTESIAN_POINT('Origin',(-24.92755355845,-89.5,16.1978257430375));
#14590=CARTESIAN_POINT('Origin',(-25.6346603396366,-89.5,16.904932524224));
#14591=CARTESIAN_POINT('Origin',(-64.5,-89.5,19.5));
#14592=CARTESIAN_POINT('',(-64.5,-89.5,20.));
#14593=CARTESIAN_POINT('Origin',(-64.5,-89.5,19.5));
#14594=CARTESIAN_POINT('Origin',(-64.5,-89.5,19.5));
#14595=CARTESIAN_POINT('Origin',(-64.5,-89.5,19.5));
#14596=CARTESIAN_POINT('Origin',(-64.5,-89.5,0.));
#14597=CARTESIAN_POINT('Origin',(-23.0395928638606,89.5,19.5));
#14598=CARTESIAN_POINT('',(-22.6860394732673,89.5,19.1464466094067));
#14599=CARTESIAN_POINT('',(-23.0395928638606,89.5,20.));
#14600=CARTESIAN_POINT('Origin',(-23.0395928638606,89.5,19.5));
#14601=CARTESIAN_POINT('Origin',(-23.0395928638606,89.5,19.5));
#14602=CARTESIAN_POINT('Origin',(-23.0395928638606,89.5,19.5));
#14603=CARTESIAN_POINT('Origin',(-5.47791795259883,89.5,37.0616749112618));
#14604=CARTESIAN_POINT('',(-5.12436456200555,89.5,36.7081215206685));
#14605=CARTESIAN_POINT('Origin',(32.5,89.5,19.5));
#14606=CARTESIAN_POINT('',(32.5,89.5,20.));
#14607=CARTESIAN_POINT('Origin',(-23.0395928638606,-89.5,19.5));
#14608=CARTESIAN_POINT('',(-22.6860394732673,-89.5,19.1464466094067));
#14609=CARTESIAN_POINT('Origin',(-23.0395928638606,-89.5,19.5));
#14610=CARTESIAN_POINT('',(-23.0395928638606,-89.5,20.));
#14611=CARTESIAN_POINT('Origin',(-23.0395928638606,-89.5,19.5));
#14612=CARTESIAN_POINT('Origin',(-23.0395928638606,-89.5,19.5));
#14613=CARTESIAN_POINT('Origin',(-23.0395928638606,-45.,19.5));
#14614=CARTESIAN_POINT('',(-23.0395928638606,-45.,20.));
#14615=CARTESIAN_POINT('',(-22.6860394732673,-45.,19.1464466094067));
#14616=CARTESIAN_POINT('Origin',(-32.5,-89.5,19.5));
#14617=CARTESIAN_POINT('',(-32.5,-89.5,20.));
#14618=CARTESIAN_POINT('Origin',(-37.9779179525988,-89.5,4.56167491126179));
#14619=CARTESIAN_POINT('',(-37.6243645620056,-89.5,4.20812152066852));
#14620=CARTESIAN_POINT('Origin',(-64.5,45.,19.5));
#14621=CARTESIAN_POINT('',(-64.5,45.,20.));
#14622=CARTESIAN_POINT('Origin',(-45.5673301698183,-89.5,15.1978257430375));
#14623=CARTESIAN_POINT('',(-45.5673301698183,-89.5,15.6978257430375));
#14624=CARTESIAN_POINT('Origin',(-24.92755355845,-90.,16.1978257430375));
#14625=CARTESIAN_POINT('',(-24.92755355845,-90.,15.6978257430375));
#14626=CARTESIAN_POINT('',(-25.2811069490433,-90.,16.5513791336308));
#14627=CARTESIAN_POINT('Origin',(19.4326698301817,89.5,15.1978257430375));
#14628=CARTESIAN_POINT('',(19.4326698301817,89.5,15.6978257430375));
#14629=CARTESIAN_POINT('Origin',(-19.5453000725091,89.5,7.84891287151875));
#14630=CARTESIAN_POINT('',(-19.045300072509,89.5,7.84891287151875));
#14631=CARTESIAN_POINT('Origin',(22.9773499637455,89.5,3.19782574303749));
#14632=CARTESIAN_POINT('',(22.9773499637455,89.5,3.69782574303749));
#14633=CARTESIAN_POINT('Origin',(64.5,-45.,19.5));
#14634=CARTESIAN_POINT('',(64.5,-45.,20.));
#14635=CARTESIAN_POINT('Origin',(-32.5,-89.5,19.5));
#14636=CARTESIAN_POINT('',(-32.5,-89.5,20.));
#14637=CARTESIAN_POINT('Origin',(32.5,89.5,19.5));
#14638=CARTESIAN_POINT('',(32.5,89.5,20.));
#14639=CARTESIAN_POINT('Origin',(22.0741207385024,89.5,1.84891287151875));
#14640=CARTESIAN_POINT('',(21.5741207385024,89.5,1.84891287151875));
#14641=CARTESIAN_POINT('Origin',(43.2870603692512,89.5,15.1978257430375));
#14642=CARTESIAN_POINT('',(43.2870603692512,89.5,15.6978257430375));
#14643=CARTESIAN_POINT('Origin',(44.3272645584125,-90.,16.1978257430375));
#14644=CARTESIAN_POINT('',(44.8272645584125,-90.,16.1978257430375));
#14645=CARTESIAN_POINT('',(44.3272645584125,-90.,15.6978257430375));
#14646=CARTESIAN_POINT('Origin',(0.,0.,0.));
#14647=CARTESIAN_POINT('Origin',(44.8272645584125,-90.,15.6978257430375));
#14648=CARTESIAN_POINT('Origin',(21.5741207385024,-90.,15.6978257430375));
#14649=CARTESIAN_POINT('Origin',(21.5741207385024,-90.,3.69782574303749));
#14650=CARTESIAN_POINT('Origin',(-19.045300072509,-90.,3.69782574303749));
#14651=CARTESIAN_POINT('Origin',(-19.045300072509,-90.,15.6978257430375));
#14652=CARTESIAN_POINT('Origin',(-26.1346603396366,-90.,15.6978257430375));
#14653=CARTESIAN_POINT('Origin',(-65.,90.,0.));
#14654=CARTESIAN_POINT('Origin',(-21.8324860826741,-90.,20.));
#14655=CARTESIAN_POINT('Origin',(0.,0.,20.));
#14656=CARTESIAN_POINT('Origin',(0.,0.,20.));
#17815=UNCERTAINTY_MEASURE_WITH_UNIT(LENGTH_MEASURE(0.01),#17837,
'DISTANCE_ACCURACY_VALUE',
'Maximum model space distance between geometric entities at asserted c
onnectivities');
#17824=UNCERTAINTY_MEASURE_WITH_UNIT(LENGTH_MEASURE(0.01),#17837,
'DISTANCE_ACCURACY_VALUE',
'Maximum model space distance between geometric entities at asserted c
onnectivities');
#17827=(
GEOMETRIC_REPRESENTATION_CONTEXT(3)
GLOBAL_UNCERTAINTY_ASSIGNED_CONTEXT((#17815))
GLOBAL_UNIT_ASSIGNED_CONTEXT((#17837,#17839,#17840))
REPRESENTATION_CONTEXT('','3D')
);
#17836=(
GEOMETRIC_REPRESENTATION_CONTEXT(3)
GLOBAL_UNCERTAINTY_ASSIGNED_CONTEXT((#17824))
GLOBAL_UNIT_ASSIGNED_CONTEXT((#17837,#17839,#17840))
REPRESENTATION_CONTEXT('','3D')
);
#17837=(
LENGTH_UNIT()
NAMED_UNIT(*)
SI_UNIT(.MILLI.,.METRE.)
);
#17839=(
NAMED_UNIT(*)
PLANE_ANGLE_UNIT()
SI_UNIT($,.RADIAN.)
);
#17840=(
NAMED_UNIT(*)
SI_UNIT($,.STERADIAN.)
SOLID_ANGLE_UNIT()
);
#17843=SHAPE_DEFINITION_REPRESENTATION(#17854,#17875);
#17854=PRODUCT_DEFINITION_SHAPE('',$,#17887);
#17875=SHAPE_REPRESENTATION('',(#9764),#17827);
#17884=PRODUCT_DEFINITION_CONTEXT('part definition',#17919,'design');
#17887=PRODUCT_DEFINITION('Bottom_Plate','Bottom_Plate',#17898,#17884);
#17898=PRODUCT_DEFINITION_FORMATION('',$,#17923);
#17919=APPLICATION_CONTEXT(
'Core Data for Automotive Mechanical Design Process');
#17920=PRODUCT_CONTEXT('part definition',#17919,'mechanical');
#17923=PRODUCT('Bottom_Plate','Bottom_Plate',$,(#17920));
#17953=COLOUR_RGB('Light Blue',0.38,0.62,0.78);
#17954=FILL_AREA_STYLE_COLOUR('',#17953);
#17955=FILL_AREA_STYLE('',(#17954));
#17956=SURFACE_STYLE_FILL_AREA(#17955);
#17957=SURFACE_SIDE_STYLE('',(#17956));
#17958=SURFACE_STYLE_USAGE(.BOTH.,#17957);
#17959=PRESENTATION_STYLE_ASSIGNMENT((#17958));
ENDSEC;
END-ISO-10303-21;
